ISO-10303-21;
HEADER;
FILE_DESCRIPTION (('STEP AP214'),
    '1' );
FILE_NAME ('Servo-Head.step',
    '2026-11-01T05:08:46',
    ( '' ),
    ( '' ),
    'SwSTEP 2.0',
    'SolidWorks 2024',
    '' );
FILE_SCHEMA (( 'AUTOMOTIVE_DESIGN' ));
ENDSEC;

DATA;
#16=EDGE_LOOP ( 'NONE', ( #11957, #12482 ) ) ;
#37=ADVANCED_FACE ( 'NONE', ( #11495 ), #14331, .T. ) ;
#57=FACE_OUTER_BOUND ( 'NONE', #15160, .T. ) ;
#75=DIRECTION ( 'NONE',  ( -1.000000000000000000, 0.000000000000000000, 0.000000000000000000 ) ) ;
#95=DIRECTION ( 'NONE',  ( 0.000000000000000000, 0.000000000000000000, -1.000000000000000000 ) ) ;
#97=DIRECTION ( 'NONE',  ( 0.000000000000000000, 1.000000000000000000, 0.000000000000000000 ) ) ;
#119=DIRECTION ( 'NONE',  ( 0.000000000000000000, 0.000000000000000000, -1.000000000000000000 ) ) ;
#147=LINE ( 'NONE', #6904, #3585 ) ;
#149=DIRECTION ( 'NONE',  ( 0.000000000000000000, 0.000000000000000000, -1.000000000000000000 ) ) ;
#154=ORIENTED_EDGE ( 'NONE', *, *, #9509, .T. ) ;
#160=ORIENTED_EDGE ( 'NONE', *, *, #15589, .F. ) ;
#161=ADVANCED_FACE ( 'NONE', ( #5735 ), #14936, .F. ) ;
#185=CIRCLE ( 'NONE', #2363, 35.00000000000000711 ) ;
#196=ORIENTED_EDGE ( 'NONE', *, *, #11498, .T. ) ;
#209=CARTESIAN_POINT ( 'NONE',  ( -40.00000000000000000, 19.00000000000000000, 25.99999999999999645 ) ) ;
#211=ORIENTED_EDGE ( 'NONE', *, *, #12141, .T. ) ;
#224=PLANE ( 'NONE',  #3358 ) ;
#232=DIRECTION ( 'NONE',  ( -1.000000000000000000, -0.000000000000000000, -0.000000000000000000 ) ) ;
#236=VECTOR ( 'NONE', #1676, 1000.000000000000000 ) ;
#245=EDGE_CURVE ( 'NONE', #1755, #1411, #11552, .T. ) ;
#251=DIRECTION ( 'NONE',  ( -0.000000000000000000, -1.000000000000000000, -0.000000000000000000 ) ) ;
#259=EDGE_CURVE ( 'NONE', #12691, #4652, #11398, .T. ) ;
#264=EDGE_CURVE ( 'NONE', #8649, #6752, #7174, .T. ) ;
#265=AXIS2_PLACEMENT_3D ( 'NONE', #2009, #9585, #7241 ) ;
#267=DIRECTION ( 'NONE',  ( -0.000000000000000000, -1.000000000000000000, -0.000000000000000000 ) ) ;
#279=CARTESIAN_POINT ( 'NONE',  ( -31.00000000000000000, 19.00000000000000000, 30.99999999999999289 ) ) ;
#282=ORIENTED_EDGE ( 'NONE', *, *, #350, .F. ) ;
#290=DIRECTION ( 'NONE',  ( 1.000000000000000000, 0.000000000000000000, 0.000000000000000000 ) ) ;
#292=EDGE_LOOP ( 'NONE', ( #15746, #13221 ) ) ;
#296=LINE ( 'NONE', #13440, #11603 ) ;
#298=CARTESIAN_POINT ( 'NONE',  ( 31.00000000000003553, 19.00000000000000000, 20.99999999999999289 ) ) ;
#313=DIRECTION ( 'NONE',  ( 0.000000000000000000, 0.000000000000000000, -1.000000000000000000 ) ) ;
#316=CARTESIAN_POINT ( 'NONE',  ( 31.81980515339464333, 8.000000000000000000, -31.81980515339463622 ) ) ;
#324=DIRECTION ( 'NONE',  ( 0.000000000000000000, 1.000000000000000000, -0.000000000000000000 ) ) ;
#328=FACE_OUTER_BOUND ( 'NONE', #16951, .T. ) ;
#331=CARTESIAN_POINT ( 'NONE',  ( -40.00000000000000000, 19.00000000000000000, 25.99999999999999645 ) ) ;
#350=EDGE_CURVE ( 'NONE', #7005, #8783, #2806, .T. ) ;
#358=ORIENTED_EDGE ( 'NONE', *, *, #6976, .T. ) ;
#370=DIRECTION ( 'NONE',  ( 0.000000000000000000, 0.000000000000000000, 1.000000000000000000 ) ) ;
#394=VERTEX_POINT ( 'NONE', #12853 ) ;
#395=ORIENTED_EDGE ( 'NONE', *, *, #13293, .F. ) ;
#398=CARTESIAN_POINT ( 'NONE',  ( 35.00000000000000711, 19.00000000000000000, -21.00000000000000355 ) ) ;
#403=DIRECTION ( 'NONE',  ( -0.000000000000000000, -1.000000000000000000, -0.000000000000000000 ) ) ;
#421=CARTESIAN_POINT ( 'NONE',  ( 21.00000000000000000, 19.00000000000000000, -31.00000000000003908 ) ) ;
#454=EDGE_LOOP ( 'NONE', ( #6809, #515, #4102, #6359 ) ) ;
#469=DIRECTION ( 'NONE',  ( -0.000000000000000000, -1.000000000000000000, -0.000000000000000000 ) ) ;
#471=ORIENTED_EDGE ( 'NONE', *, *, #2752, .T. ) ;
#474=ORIENTED_EDGE ( 'NONE', *, *, #3207, .F. ) ;
#483=DIRECTION ( 'NONE',  ( 0.000000000000000000, -0.000000000000000000, -1.000000000000000000 ) ) ;
#487=ADVANCED_FACE ( 'NONE', ( #11733 ), #3920, .F. ) ;
#492=CARTESIAN_POINT ( 'NONE',  ( 31.00000000000003908, 19.00000000000000000, -26.00000000000000355 ) ) ;
#495=ORIENTED_EDGE ( 'NONE', *, *, #7517, .F. ) ;
#499=CARTESIAN_POINT ( 'NONE',  ( -26.00000000000000000, 19.00000000000000000, 40.00000000000001421 ) ) ;
#515=ORIENTED_EDGE ( 'NONE', *, *, #5284, .F. ) ;
#518=VECTOR ( 'NONE', #5837, 1000.000000000000000 ) ;
#519=CARTESIAN_POINT ( 'NONE',  ( -40.00000000000000000, 19.00000000000000000, -26.00000000000000355 ) ) ;
#526=CARTESIAN_POINT ( 'NONE',  ( 26.00000000000000000, 11.00000000000000000, 31.00000000000003197 ) ) ;
#534=ORIENTED_EDGE ( 'NONE', *, *, #4637, .T. ) ;
#538=EDGE_LOOP ( 'NONE', ( #7042, #495 ) ) ;
#564=VECTOR ( 'NONE', #16813, 1000.000000000000000 ) ;
#566=EDGE_CURVE ( 'NONE', #4897, #14008, #2886, .T. ) ;
#570=DIRECTION ( 'NONE',  ( -0.000000000000000000, -1.000000000000000000, -0.000000000000000000 ) ) ;
#590=CARTESIAN_POINT ( 'NONE',  ( -39.99999999999999289, 0.000000000000000000, 34.99999999999997868 ) ) ;
#596=EDGE_CURVE ( 'NONE', #7827, #13441, #12258, .T. ) ;
#597=VECTOR ( 'NONE', #10608, 1000.000000000000000 ) ;
#598=EDGE_CURVE ( 'NONE', #16829, #7102, #9508, .T. ) ;
#600=EDGE_CURVE ( 'NONE', #13441, #16829, #10788, .T. ) ;
#602=LINE ( 'NONE', #519, #12957 ) ;
#603=EDGE_LOOP ( 'NONE', ( #196, #16739, #1318, #8530 ) ) ;
#605=VECTOR ( 'NONE', #290, 1000.000000000000000 ) ;
#615=EDGE_CURVE ( 'NONE', #2722, #903, #6909, .T. ) ;
#625=CARTESIAN_POINT ( 'NONE',  ( -35.00000000000000000, 8.000000000000000000, 20.99999999999999289 ) ) ;
#638=ORIENTED_EDGE ( 'NONE', *, *, #2734, .T. ) ;
#641=FACE_OUTER_BOUND ( 'NONE', #9058, .T. ) ;
#645=AXIS2_PLACEMENT_3D ( 'NONE', #7793, #11580, #1282 ) ;
#657=EDGE_LOOP ( 'NONE', ( #14248, #4305, #2695, #5890, #6096, #3804 ) ) ;
#674=ORIENTED_EDGE ( 'NONE', *, *, #12126, .F. ) ;
#679=AXIS2_PLACEMENT_3D ( 'NONE', #15816, #4055, #2757 ) ;
#686=EDGE_CURVE ( 'NONE', #12698, #1954, #7153, .T. ) ;
#695=EDGE_CURVE ( 'NONE', #7005, #1870, #905, .T. ) ;
#704=DIRECTION ( 'NONE',  ( 0.000000000000000000, 0.000000000000000000, 1.000000000000000000 ) ) ;
#731=ORIENTED_EDGE ( 'NONE', *, *, #9384, .T. ) ;
#734=DIRECTION ( 'NONE',  ( -0.000000000000000000, -1.000000000000000000, -0.000000000000000000 ) ) ;
#742=VERTEX_POINT ( 'NONE', #11208 ) ;
#747=VERTEX_POINT ( 'NONE', #8726 ) ;
#749=DIRECTION ( 'NONE',  ( -0.000000000000000000, -1.000000000000000000, -0.000000000000000000 ) ) ;
#775=CARTESIAN_POINT ( 'NONE',  ( 0.000000000000000000, 0.000000000000000000, 35.00000000000000711 ) ) ;
#789=AXIS2_PLACEMENT_3D ( 'NONE', #11450, #8719, #7571 ) ;
#797=CARTESIAN_POINT ( 'NONE',  ( -20.99999999999999645, 19.00000000000000000, 35.00000000000001421 ) ) ;
#803=ORIENTED_EDGE ( 'NONE', *, *, #3451, .T. ) ;
#806=EDGE_CURVE ( 'NONE', #9059, #6790, #3566, .T. ) ;
#815=VECTOR ( 'NONE', #5478, 1000.000000000000000 ) ;
#825=ORIENTED_EDGE ( 'NONE', *, *, #2966, .F. ) ;
#830=EDGE_LOOP ( 'NONE', ( #7966, #6621, #16449, #9149 ) ) ;
#835=ORIENTED_EDGE ( 'NONE', *, *, #11748, .T. ) ;
#845=DIRECTION ( 'NONE',  ( -1.000000000000000000, 0.000000000000000000, -0.000000000000000000 ) ) ;
#861=VECTOR ( 'NONE', #12744, 1000.000000000000000 ) ;
#869=ORIENTED_EDGE ( 'NONE', *, *, #1177, .T. ) ;
#870=EDGE_CURVE ( 'NONE', #15712, #4694, #11591, .T. ) ;
#872=CARTESIAN_POINT ( 'NONE',  ( -40.00000000000000000, 19.00000000000000000, 25.99999999999999645 ) ) ;
#900=EDGE_CURVE ( 'NONE', #13213, #10460, #15909, .T. ) ;
#903=VERTEX_POINT ( 'NONE', #9572 ) ;
#905=LINE ( 'NONE', #6125, #13249 ) ;
#909=AXIS2_PLACEMENT_3D ( 'NONE', #13908, #2132, #7360 ) ;
#910=DIRECTION ( 'NONE',  ( 0.000000000000000000, 1.000000000000000000, 0.000000000000000000 ) ) ;
#915=DIRECTION ( 'NONE',  ( 0.000000000000000000, 0.000000000000000000, -1.000000000000000000 ) ) ;
#927=VECTOR ( 'NONE', #2862, 1000.000000000000000 ) ;
#930=CARTESIAN_POINT ( 'NONE',  ( 35.00000000000000711, 8.000000000000000000, 35.00000000000000711 ) ) ;
#937=CIRCLE ( 'NONE', #10530, 3.300000000000000711 ) ;
#939=VECTOR ( 'NONE', #7634, 1000.000000000000000 ) ;
#949=DIRECTION ( 'NONE',  ( 0.000000000000000000, 0.000000000000000000, -1.000000000000000000 ) ) ;
#961=DIRECTION ( 'NONE',  ( 0.000000000000000000, 0.000000000000000000, 1.000000000000000000 ) ) ;
#967=CIRCLE ( 'NONE', #2876, 3.300000000000000711 ) ;
#970=ORIENTED_EDGE ( 'NONE', *, *, #1566, .F. ) ;
#978=DIRECTION ( 'NONE',  ( -0.000000000000000000, -1.000000000000000000, -0.000000000000000000 ) ) ;
#981=LINE ( 'NONE', #8797, #5291 ) ;
#987=DIRECTION ( 'NONE',  ( 0.000000000000000000, 0.000000000000000000, -1.000000000000000000 ) ) ;
#1021=EDGE_CURVE ( 'NONE', #2369, #7414, #12312, .T. ) ;
#1024=CARTESIAN_POINT ( 'NONE',  ( -20.99999999999999645, 8.000000000000000000, -31.00000000000003908 ) ) ;
#1052=CARTESIAN_POINT ( 'NONE',  ( -31.81980515339462912, 11.00000000000000000, 35.11980515339465825 ) ) ;
#1055=ORIENTED_EDGE ( 'NONE', *, *, #1441, .F. ) ;
#1063=CARTESIAN_POINT ( 'NONE',  ( 31.81980515339464333, 0.000000000000000000, 35.11980515339463693 ) ) ;
#1065=DIRECTION ( 'NONE',  ( 0.000000000000000000, -0.000000000000000000, -1.000000000000000000 ) ) ;
#1075=CARTESIAN_POINT ( 'NONE',  ( 0.000000000000000000, 8.000000000000000000, 0.000000000000000000 ) ) ;
#1090=ORIENTED_EDGE ( 'NONE', *, *, #14104, .F. ) ;
#1100=ORIENTED_EDGE ( 'NONE', *, *, #5272, .T. ) ;
#1122=CYLINDRICAL_SURFACE ( 'NONE', #13462, 4.999999999999997335 ) ;
#1127=ORIENTED_EDGE ( 'NONE', *, *, #598, .T. ) ;
#1129=ADVANCED_FACE ( 'NONE', ( #3135 ), #8370, .F. ) ;
#1134=ORIENTED_EDGE ( 'NONE', *, *, #9509, .F. ) ;
#1135=VECTOR ( 'NONE', #13366, 1000.000000000000000 ) ;
#1136=ORIENTED_EDGE ( 'NONE', *, *, #14537, .T. ) ;
#1161=AXIS2_PLACEMENT_3D ( 'NONE', #3082, #13571, #9788 ) ;
#1164=VECTOR ( 'NONE', #10012, 1000.000000000000000 ) ;
#1177=EDGE_CURVE ( 'NONE', #10479, #13438, #7704, .T. ) ;
#1191=CARTESIAN_POINT ( 'NONE',  ( -35.00000000000000000, 19.00000000000000000, 20.99999999999999289 ) ) ;
#1213=PLANE ( 'NONE',  #3581 ) ;
#1221=EDGE_LOOP ( 'NONE', ( #1972, #9774, #15434, #5511 ) ) ;
#1222=DIRECTION ( 'NONE',  ( 0.000000000000000000, 0.000000000000000000, -1.000000000000000000 ) ) ;
#1224=AXIS2_PLACEMENT_3D ( 'NONE', #279, #10924, #8345 ) ;
#1230=ADVANCED_FACE ( 'NONE', ( #13135 ), #10307, .F. ) ;
#1231=CARTESIAN_POINT ( 'NONE',  ( 26.00000000000000355, 19.00000000000000000, -31.00000000000004263 ) ) ;
#1238=ORIENTED_EDGE ( 'NONE', *, *, #14526, .F. ) ;
#1239=FACE_OUTER_BOUND ( 'NONE', #11636, .T. ) ;
#1267=CARTESIAN_POINT ( 'NONE',  ( -31.00000000000006395, 19.00000000000000000, 20.99999999999998934 ) ) ;
#1281=CARTESIAN_POINT ( 'NONE',  ( 34.99999999999997868, 8.000000000000000000, 40.00000000000000711 ) ) ;
#1282=DIRECTION ( 'NONE',  ( 1.000000000000000000, 0.000000000000000000, -0.000000000000000000 ) ) ;
#1285=DIRECTION ( 'NONE',  ( -0.000000000000000000, -1.000000000000000000, -0.000000000000000000 ) ) ;
#1306=ORIENTED_EDGE ( 'NONE', *, *, #10791, .T. ) ;
#1310=ADVANCED_FACE ( 'NONE', ( #13318 ), #9534, .T. ) ;
#1313=AXIS2_PLACEMENT_3D ( 'NONE', #3228, #8285, #13540 ) ;
#1318=ORIENTED_EDGE ( 'NONE', *, *, #16935, .F. ) ;
#1324=EDGE_CURVE ( 'NONE', #2054, #11526, #1422, .T. ) ;
#1350=CARTESIAN_POINT ( 'NONE',  ( 4.286263797015737285E-15, -3.000000000000000000, -35.00000000000000711 ) ) ;
#1364=DIRECTION ( 'NONE',  ( 1.000000000000000000, -0.000000000000000000, 0.000000000000000000 ) ) ;
#1373=CYLINDRICAL_SURFACE ( 'NONE', #5059, 9.999999999999998224 ) ;
#1396=ORIENTED_EDGE ( 'NONE', *, *, #9384, .F. ) ;
#1402=LINE ( 'NONE', #298, #15818 ) ;
#1411=VERTEX_POINT ( 'NONE', #13191 ) ;
#1422=CIRCLE ( 'NONE', #15411, 35.00000000000000711 ) ;
#1435=AXIS2_PLACEMENT_3D ( 'NONE', #7710, #7888, #7399 ) ;
#1441=EDGE_CURVE ( 'NONE', #10521, #4694, #2531, .T. ) ;
#1445=ORIENTED_EDGE ( 'NONE', *, *, #14104, .T. ) ;
#1457=DIRECTION ( 'NONE',  ( 1.000000000000000000, 0.000000000000000000, 0.000000000000000000 ) ) ;
#1478=ORIENTED_EDGE ( 'NONE', *, *, #5200, .T. ) ;
#1488=AXIS2_PLACEMENT_3D ( 'NONE', #3280, #8693, #15217 ) ;
#1491=AXIS2_PLACEMENT_3D ( 'NONE', #16666, #5064, #16910 ) ;
#1499=ORIENTED_EDGE ( 'NONE', *, *, #3451, .F. ) ;
#1541=CARTESIAN_POINT ( 'NONE',  ( 0.000000000000000000, -3.000000000000000000, 0.000000000000000000 ) ) ;
#1544=EDGE_CURVE ( 'NONE', #10621, #1954, #3053, .T. ) ;
#1549=EDGE_CURVE ( 'NONE', #13438, #10961, #4514, .T. ) ;
#1550=CARTESIAN_POINT ( 'NONE',  ( -26.00000000000000000, 19.00000000000000000, 40.00000000000001421 ) ) ;
#1561=VERTEX_POINT ( 'NONE', #9837 ) ;
#1566=EDGE_CURVE ( 'NONE', #11526, #2054, #6796, .T. ) ;
#1569=VECTOR ( 'NONE', #15501, 1000.000000000000000 ) ;
#1573=CARTESIAN_POINT ( 'NONE',  ( 35.00000000000000711, 19.00000000000000000, 20.99999999999999289 ) ) ;
#1579=ORIENTED_EDGE ( 'NONE', *, *, #3732, .F. ) ;
#1580=AXIS2_PLACEMENT_3D ( 'NONE', #12541, #13837, #16575 ) ;
#1581=DIRECTION ( 'NONE',  ( -0.000000000000000000, -1.000000000000000000, -0.000000000000000000 ) ) ;
#1589=DIRECTION ( 'NONE',  ( -0.000000000000000000, -0.000000000000000000, 1.000000000000000000 ) ) ;
#1600=CARTESIAN_POINT ( 'NONE',  ( 31.81980515339464333, 0.000000000000000000, 28.51980515339463906 ) ) ;
#1607=CARTESIAN_POINT ( 'NONE',  ( 26.00000000000000355, 19.00000000000000000, -31.00000000000003908 ) ) ;
#1612=ORIENTED_EDGE ( 'NONE', *, *, #2734, .F. ) ;
#1616=ORIENTED_EDGE ( 'NONE', *, *, #245, .T. ) ;
#1624=ORIENTED_EDGE ( 'NONE', *, *, #4255, .F. ) ;
#1627=EDGE_CURVE ( 'NONE', #8729, #9952, #15064, .T. ) ;
#1646=DIRECTION ( 'NONE',  ( -3.854941057726247958E-16, 0.000000000000000000, 1.000000000000000000 ) ) ;
#1659=EDGE_CURVE ( 'NONE', #9059, #747, #4069, .T. ) ;
#1665=DIRECTION ( 'NONE',  ( -0.000000000000000000, -1.000000000000000000, -0.000000000000000000 ) ) ;
#1669=DIRECTION ( 'NONE',  ( 0.000000000000000000, 1.000000000000000000, 0.000000000000000000 ) ) ;
#1671=ORIENTED_EDGE ( 'NONE', *, *, #6132, .T. ) ;
#1676=DIRECTION ( 'NONE',  ( -0.000000000000000000, -1.000000000000000000, -0.000000000000000000 ) ) ;
#1686=EDGE_LOOP ( 'NONE', ( #4706, #4435, #4885, #9982 ) ) ;
#1687=DIRECTION ( 'NONE',  ( -3.854941057726250916E-16, 0.000000000000000000, -1.000000000000000000 ) ) ;
#1694=AXIS2_PLACEMENT_3D ( 'NONE', #15698, #3945, #9187 ) ;
#1695=AXIS2_PLACEMENT_3D ( 'NONE', #1075, #3909, #2275 ) ;
#1712=( NAMED_UNIT ( * ) SI_UNIT ( $, .STERADIAN. ) SOLID_ANGLE_UNIT ( ) );
#1719=VERTEX_POINT ( 'NONE', #6033 ) ;
#1721=VECTOR ( 'NONE', #8206, 1000.000000000000000 ) ;
#1733=ORIENTED_EDGE ( 'NONE', *, *, #3415, .T. ) ;
#1743=FACE_BOUND ( 'NONE', #9478, .T. ) ;
#1744=LINE ( 'NONE', #6010, #6960 ) ;
#1751=AXIS2_PLACEMENT_3D ( 'NONE', #11035, #5792, #3561 ) ;
#1755=VERTEX_POINT ( 'NONE', #10003 ) ;
#1756=FACE_OUTER_BOUND ( 'NONE', #15388, .T. ) ;
#1765=EDGE_CURVE ( 'NONE', #903, #11543, #6504, .T. ) ;
#1772=FACE_OUTER_BOUND ( 'NONE', #16, .T. ) ;
#1790=ORIENTED_EDGE ( 'NONE', *, *, #806, .F. ) ;
#1794=CARTESIAN_POINT ( 'NONE',  ( 40.00000000000000711, 8.000000000000000000, 34.99999999999997868 ) ) ;
#1795=AXIS2_PLACEMENT_3D ( 'NONE', #8157, #16139, #16056 ) ;
#1805=AXIS2_PLACEMENT_3D ( 'NONE', #11292, #7501, #11381 ) ;
#1814=LINE ( 'NONE', #16322, #4622 ) ;
#1820=DIRECTION ( 'NONE',  ( 0.000000000000000000, 1.000000000000000000, 0.000000000000000000 ) ) ;
#1823=DIRECTION ( 'NONE',  ( 0.000000000000000000, 0.000000000000000000, 1.000000000000000000 ) ) ;
#1833=EDGE_LOOP ( 'NONE', ( #5101, #674, #2755, #13871, #16472, #6204, #15110, #16079 ) ) ;
#1839=VERTEX_POINT ( 'NONE', #9283 ) ;
#1845=ORIENTED_EDGE ( 'NONE', *, *, #4685, .F. ) ;
#1870=VERTEX_POINT ( 'NONE', #10832 ) ;
#1880=CARTESIAN_POINT ( 'NONE',  ( 31.81980515339464333, 0.000000000000000000, -28.51980515339463906 ) ) ;
#1884=SURFACE_SIDE_STYLE ('',( #12200 ) ) ;
#1896=DIRECTION ( 'NONE',  ( 0.000000000000000000, -1.000000000000000000, 0.000000000000000000 ) ) ;
#1900=CARTESIAN_POINT ( 'NONE',  ( 35.00000000000000711, 19.00000000000000000, -21.00000000000000355 ) ) ;
#1915=ORIENTED_EDGE ( 'NONE', *, *, #6592, .T. ) ;
#1942=EDGE_CURVE ( 'NONE', #5920, #13660, #4708, .T. ) ;
#1943=DIRECTION ( 'NONE',  ( 0.000000000000000000, 1.000000000000000000, 0.000000000000000000 ) ) ;
#1944=FACE_OUTER_BOUND ( 'NONE', #14445, .T. ) ;
#1954=VERTEX_POINT ( 'NONE', #1970 ) ;
#1956=CARTESIAN_POINT ( 'NONE',  ( 0.000000000000000000, -3.000000000000000000, -18.50000000000000000 ) ) ;
#1962=CIRCLE ( 'NONE', #1695, 18.50000000000000000 ) ;
#1970=CARTESIAN_POINT ( 'NONE',  ( 40.00000000000000711, 11.00000000000000000, 25.99999999999999645 ) ) ;
#1971=DIRECTION ( 'NONE',  ( 0.000000000000000000, 0.000000000000000000, 1.000000000000000000 ) ) ;
#1972=ORIENTED_EDGE ( 'NONE', *, *, #16844, .T. ) ;
#1993=EDGE_CURVE ( 'NONE', #6752, #5994, #15031, .T. ) ;
#2004=LINE ( 'NONE', #7236, #6944 ) ;
#2008=CARTESIAN_POINT ( 'NONE',  ( -20.99999999999999645, 19.00000000000000000, -31.00000000000003908 ) ) ;
#2009=CARTESIAN_POINT ( 'NONE',  ( 0.000000000000000000, 8.000000000000000000, 0.000000000000000000 ) ) ;
#2015=EDGE_CURVE ( 'NONE', #7006, #11353, #1814, .T. ) ;
#2020=CARTESIAN_POINT ( 'NONE',  ( -39.99999999999999289, 11.00000000000000000, -26.00000000000000355 ) ) ;
#2038=AXIS2_PLACEMENT_3D ( 'NONE', #7707, #1285, #6500 ) ;
#2054=VERTEX_POINT ( 'NONE', #14953 ) ;
#2099=CARTESIAN_POINT ( 'NONE',  ( 21.00000000000000000, 19.00000000000000000, 35.00000000000001421 ) ) ;
#2128=CARTESIAN_POINT ( 'NONE',  ( 21.00000000000000000, 19.00000000000000000, 35.00000000000001421 ) ) ;
#2132=DIRECTION ( 'NONE',  ( 1.000000000000000000, -0.000000000000000000, 0.000000000000000000 ) ) ;
#2151=EDGE_CURVE ( 'NONE', #16324, #5994, #12953, .T. ) ;
#2155=LINE ( 'NONE', #6423, #939 ) ;
#2156=ORIENTED_EDGE ( 'NONE', *, *, #14025, .F. ) ;
#2164=VERTEX_POINT ( 'NONE', #3854 ) ;
#2170=FACE_OUTER_BOUND ( 'NONE', #11247, .T. ) ;
#2181=LINE ( 'NONE', #16524, #10342 ) ;
#2183=ADVANCED_BREP_SHAPE_REPRESENTATION ( '', ( #14480, #1488 ), #15199 ) ;
#2208=AXIS2_PLACEMENT_3D ( 'NONE', #8137, #1943, #9522 ) ;
#2211=ORIENTED_EDGE ( 'NONE', *, *, #870, .F. ) ;
#2212=CARTESIAN_POINT ( 'NONE',  ( -35.00000000000000000, 19.00000000000000000, 20.99999999999999289 ) ) ;
#2239=CARTESIAN_POINT ( 'NONE',  ( -40.00000000000000000, 19.00000000000000000, -26.00000000000000355 ) ) ;
#2240=EDGE_LOOP ( 'NONE', ( #4765, #9169, #16586, #8598, #11088, #1134, #16842, #10933, #16427, #4181, #14712, #10577, #7465, #12643, #6008, #16320 ) ) ;
#2246=EDGE_CURVE ( 'NONE', #7889, #13660, #2561, .T. ) ;
#2265=CARTESIAN_POINT ( 'NONE',  ( 31.00000000000000000, 19.00000000000000000, -21.00000000000000355 ) ) ;
#2275=DIRECTION ( 'NONE',  ( 0.000000000000000000, 0.000000000000000000, -1.000000000000000000 ) ) ;
#2291=EDGE_CURVE ( 'NONE', #1561, #16924, #16026, .T. ) ;
#2295=CARTESIAN_POINT ( 'NONE',  ( -31.81980515339462912, 0.000000000000000000, -28.51980515339464972 ) ) ;
#2303=ADVANCED_FACE ( 'NONE', ( #10957 ), #12328, .F. ) ;
#2305=ORIENTED_EDGE ( 'NONE', *, *, #2246, .T. ) ;
#2307=VECTOR ( 'NONE', #5057, 1000.000000000000000 ) ;
#2314=ORIENTED_EDGE ( 'NONE', *, *, #1324, .F. ) ;
#2315=CARTESIAN_POINT ( 'NONE',  ( 34.99999999999997868, 8.000000000000000000, -40.00000000000000711 ) ) ;
#2329=DIRECTION ( 'NONE',  ( 0.000000000000000000, 0.000000000000000000, 1.000000000000000000 ) ) ;
#2331=ORIENTED_EDGE ( 'NONE', *, *, #9144, .T. ) ;
#2356=LINE ( 'NONE', #6131, #16867 ) ;
#2363=AXIS2_PLACEMENT_3D ( 'NONE', #6303, #2627, #15673 ) ;
#2369=VERTEX_POINT ( 'NONE', #4595 ) ;
#2381=EDGE_CURVE ( 'NONE', #7827, #7102, #11205, .T. ) ;
#2389=EDGE_LOOP ( 'NONE', ( #9364, #5145, #10593, #15478 ) ) ;
#2412=VERTEX_POINT ( 'NONE', #13957 ) ;
#2420=DIRECTION ( 'NONE',  ( -0.000000000000000000, -1.000000000000000000, -0.000000000000000000 ) ) ;
#2422=ORIENTED_EDGE ( 'NONE', *, *, #1627, .T. ) ;
#2442=VERTEX_POINT ( 'NONE', #8542 ) ;
#2444=DIRECTION ( 'NONE',  ( 0.000000000000000000, 0.000000000000000000, -1.000000000000000000 ) ) ;
#2457=EDGE_CURVE ( 'NONE', #14614, #16035, #3395, .T. ) ;
#2466=CARTESIAN_POINT ( 'NONE',  ( 34.99999999999997868, 11.00000000000000000, -40.00000000000000711 ) ) ;
#2482=DIRECTION ( 'NONE',  ( 0.000000000000000000, 0.000000000000000000, -1.000000000000000000 ) ) ;
#2487=CARTESIAN_POINT ( 'NONE',  ( -26.00000000000000000, 11.00000000000000000, 40.00000000000000711 ) ) ;
#2500=ORIENTED_EDGE ( 'NONE', *, *, #13369, .T. ) ;
#2506=CARTESIAN_POINT ( 'NONE',  ( 31.81980515339464333, 11.00000000000000000, 28.51980515339463906 ) ) ;
#2507=CARTESIAN_POINT ( 'NONE',  ( -31.00000000000003553, 19.00000000000000000, 25.99999999999999645 ) ) ;
#2531=LINE ( 'NONE', #9407, #7166 ) ;
#2540=DIRECTION ( 'NONE',  ( 0.000000000000000000, 1.000000000000000000, 0.000000000000000000 ) ) ;
#2551=VECTOR ( 'NONE', #4412, 1000.000000000000000 ) ;
#2561=LINE ( 'NONE', #9090, #16417 ) ;
#2578=ADVANCED_FACE ( 'NONE', ( #4920 ), #15498, .T. ) ;
#2595=AXIS2_PLACEMENT_3D ( 'NONE', #11249, #1896, #8434 ) ;
#2603=VERTEX_POINT ( 'NONE', #1063 ) ;
#2626=DIRECTION ( 'NONE',  ( 1.000000000000000000, 0.000000000000000000, 0.000000000000000000 ) ) ;
#2627=DIRECTION ( 'NONE',  ( 0.000000000000000000, -1.000000000000000000, 0.000000000000000000 ) ) ;
#2636=CARTESIAN_POINT ( 'NONE',  ( 31.00000000000006750, 19.00000000000000000, -21.00000000000000355 ) ) ;
#2661=FACE_BOUND ( 'NONE', #9856, .T. ) ;
#2682=DIRECTION ( 'NONE',  ( -0.000000000000000000, -1.000000000000000000, -0.000000000000000000 ) ) ;
#2688=ORIENTED_EDGE ( 'NONE', *, *, #14777, .F. ) ;
#2695=ORIENTED_EDGE ( 'NONE', *, *, #15747, .T. ) ;
#2697=EDGE_CURVE ( 'NONE', #11977, #14614, #296, .T. ) ;
#2700=VECTOR ( 'NONE', #5132, 1000.000000000000000 ) ;
#2701=EDGE_LOOP ( 'NONE', ( #6610, #10015, #12334, #1127, #15492, #13850 ) ) ;
#2714=CARTESIAN_POINT ( 'NONE',  ( 35.00000000000000711, 11.00000000000000000, -35.00000000000000711 ) ) ;
#2722=VERTEX_POINT ( 'NONE', #10760 ) ;
#2734=EDGE_CURVE ( 'NONE', #12218, #9656, #8003, .T. ) ;
#2752=EDGE_CURVE ( 'NONE', #7889, #4822, #4072, .T. ) ;
#2755=ORIENTED_EDGE ( 'NONE', *, *, #2381, .F. ) ;
#2757=DIRECTION ( 'NONE',  ( 0.000000000000000000, 0.000000000000000000, -1.000000000000000000 ) ) ;
#2784=EDGE_CURVE ( 'NONE', #16870, #2164, #14917, .T. ) ;
#2792=EDGE_CURVE ( 'NONE', #10404, #12229, #13855, .T. ) ;
#2798=DIRECTION ( 'NONE',  ( -1.000000000000000000, 0.000000000000000000, 0.000000000000000000 ) ) ;
#2806=CIRCLE ( 'NONE', #9941, 3.300000000000000711 ) ;
#2822=CARTESIAN_POINT ( 'NONE',  ( 0.000000000000000000, -3.000000000000000000, 0.000000000000000000 ) ) ;
#2846=AXIS2_PLACEMENT_3D ( 'NONE', #8950, #14270, #2329 ) ;
#2862=DIRECTION ( 'NONE',  ( -1.000000000000000000, -0.000000000000000000, -0.000000000000000000 ) ) ;
#2863=ORIENTED_EDGE ( 'NONE', *, *, #870, .T. ) ;
#2876=AXIS2_PLACEMENT_3D ( 'NONE', #11153, #16467, #8495 ) ;
#2878=LINE ( 'NONE', #8115, #1135 ) ;
#2882=PLANE ( 'NONE',  #4211 ) ;
#2886=LINE ( 'NONE', #8031, #8579 ) ;
#2926=CYLINDRICAL_SURFACE ( 'NONE', #14680, 9.999999999999998224 ) ;
#2966=EDGE_CURVE ( 'NONE', #7581, #4652, #4225, .T. ) ;
#2968=DIRECTION ( 'NONE',  ( -1.000000000000000000, 0.000000000000000000, 0.000000000000000000 ) ) ;
#2971=DIRECTION ( 'NONE',  ( 0.000000000000000000, 0.000000000000000000, 1.000000000000000000 ) ) ;
#2972=CARTESIAN_POINT ( 'NONE',  ( 31.00000000000003908, 19.00000000000000000, -26.00000000000000355 ) ) ;
#2981=CARTESIAN_POINT ( 'NONE',  ( 31.00000000000003553, 11.00000000000000000, 25.99999999999999645 ) ) ;
#2986=EDGE_CURVE ( 'NONE', #5602, #1719, #7768, .T. ) ;
#2998=DIRECTION ( 'NONE',  ( -0.000000000000000000, 1.000000000000000000, -0.000000000000000000 ) ) ;
#2999=ORIENTED_EDGE ( 'NONE', *, *, #6846, .T. ) ;
#3009=CARTESIAN_POINT ( 'NONE',  ( -31.00000000000006395, 8.000000000000000000, 20.99999999999998934 ) ) ;
#3014=LINE ( 'NONE', #7036, #4300 ) ;
#3053=LINE ( 'NONE', #4592, #13117 ) ;
#3058=DIRECTION ( 'NONE',  ( 0.000000000000000000, 0.000000000000000000, -1.000000000000000000 ) ) ;
#3068=AXIS2_PLACEMENT_3D ( 'NONE', #11199, #12824, #14368 ) ;
#3071=CARTESIAN_POINT ( 'NONE',  ( 31.00000000000006750, 19.00000000000000000, -21.00000000000000355 ) ) ;
#3082=CARTESIAN_POINT ( 'NONE',  ( -31.81980515339462912, 0.000000000000000000, -31.81980515339465043 ) ) ;
#3088=VECTOR ( 'NONE', #11986, 1000.000000000000000 ) ;
#3107=AXIS2_PLACEMENT_3D ( 'NONE', #421, #75, #9343 ) ;
#3116=EDGE_CURVE ( 'NONE', #8783, #7005, #937, .T. ) ;
#3117=DIRECTION ( 'NONE',  ( 1.000000000000000000, 0.000000000000000000, 0.000000000000000000 ) ) ;
#3122=FACE_BOUND ( 'NONE', #12220, .T. ) ;
#3127=DIRECTION ( 'NONE',  ( -0.000000000000000000, -0.000000000000000000, 1.000000000000000000 ) ) ;
#3135=FACE_OUTER_BOUND ( 'NONE', #3568, .T. ) ;
#3138=ORIENTED_EDGE ( 'NONE', *, *, #14332, .F. ) ;
#3163=CIRCLE ( 'NONE', #1224, 10.00000000000000178 ) ;
#3167=DIRECTION ( 'NONE',  ( 1.000000000000000000, 0.000000000000000000, -0.000000000000000000 ) ) ;
#3198=CARTESIAN_POINT ( 'NONE',  ( -26.00000000000000000, 19.00000000000000000, -31.00000000000003908 ) ) ;
#3207=EDGE_CURVE ( 'NONE', #1561, #14012, #6168, .T. ) ;
#3211=ORIENTED_EDGE ( 'NONE', *, *, #10864, .F. ) ;
#3221=EDGE_CURVE ( 'NONE', #10479, #13963, #15544, .T. ) ;
#3226=CARTESIAN_POINT ( 'NONE',  ( -34.99999999999996447, 11.00000000000000000, -40.00000000000000711 ) ) ;
#3228=CARTESIAN_POINT ( 'NONE',  ( 0.000000000000000000, -3.000000000000000000, 0.000000000000000000 ) ) ;
#3247=FACE_BOUND ( 'NONE', #292, .T. ) ;
#3280=CARTESIAN_POINT ( 'NONE',  ( 0.000000000000000000, 0.000000000000000000, 0.000000000000000000 ) ) ;
#3282=VERTEX_POINT ( 'NONE', #4032 ) ;
#3287=CARTESIAN_POINT ( 'NONE',  ( 31.00000000000003553, 8.000000000000000000, 20.99999999999999289 ) ) ;
#3302=LINE ( 'NONE', #16513, #8259 ) ;
#3331=ORIENTED_EDGE ( 'NONE', *, *, #13751, .F. ) ;
#3358=AXIS2_PLACEMENT_3D ( 'NONE', #15923, #12243, #12570 ) ;
#3366=ORIENTED_EDGE ( 'NONE', *, *, #1993, .F. ) ;
#3370=ORIENTED_EDGE ( 'NONE', *, *, #15624, .T. ) ;
#3372=CARTESIAN_POINT ( 'NONE',  ( -20.99999999999999645, 19.00000000000000000, 31.00000000000003197 ) ) ;
#3380=ORIENTED_EDGE ( 'NONE', *, *, #6661, .F. ) ;
#3382=ORIENTED_EDGE ( 'NONE', *, *, #6132, .F. ) ;
#3386=DIRECTION ( 'NONE',  ( -0.000000000000000000, -1.000000000000000000, -0.000000000000000000 ) ) ;
#3387=DIRECTION ( 'NONE',  ( 0.000000000000000000, 0.000000000000000000, -1.000000000000000000 ) ) ;
#3388=CIRCLE ( 'NONE', #1161, 3.300000000000000711 ) ;
#3390=DIRECTION ( 'NONE',  ( -0.000000000000000000, -1.000000000000000000, -0.000000000000000000 ) ) ;
#3392=LINE ( 'NONE', #10006, #16804 ) ;
#3395=LINE ( 'NONE', #2099, #11587 ) ;
#3415=EDGE_CURVE ( 'NONE', #1870, #4809, #3388, .T. ) ;
#3447=VERTEX_POINT ( 'NONE', #7176 ) ;
#3451=EDGE_CURVE ( 'NONE', #4924, #7414, #11064, .T. ) ;
#3488=CIRCLE ( 'NONE', #6481, 4.999999999999997335 ) ;
#3494=ORIENTED_EDGE ( 'NONE', *, *, #12637, .F. ) ;
#3506=ORIENTED_EDGE ( 'NONE', *, *, #1659, .T. ) ;
#3511=DIRECTION ( 'NONE',  ( 0.000000000000000000, 0.000000000000000000, -1.000000000000000000 ) ) ;
#3520=CARTESIAN_POINT ( 'NONE',  ( 34.99999999999997868, 0.000000000000000000, 40.00000000000000711 ) ) ;
#3523=CARTESIAN_POINT ( 'NONE',  ( 21.00000000000000000, 19.00000000000000000, -35.00000000000000711 ) ) ;
#3528=EDGE_LOOP ( 'NONE', ( #13846, #1579, #1612, #9578 ) ) ;
#3547=ORIENTED_EDGE ( 'NONE', *, *, #10791, .F. ) ;
#3561=DIRECTION ( 'NONE',  ( 1.000000000000000000, 0.000000000000000000, -0.000000000000000000 ) ) ;
#3565=CARTESIAN_POINT ( 'NONE',  ( -34.99999999999996447, 8.000000000000000000, -40.00000000000000711 ) ) ;
#3566=LINE ( 'NONE', #2265, #14631 ) ;
#3568=EDGE_LOOP ( 'NONE', ( #11467, #7560, #10308, #6605, #2305, #4000, #11131, #2331 ) ) ;
#3579=ADVANCED_FACE ( 'NONE', ( #7603 ), #10114, .F. ) ;
#3580=CARTESIAN_POINT ( 'NONE',  ( -35.00000000000000000, 19.00000000000000000, 20.99999999999999289 ) ) ;
#3581=AXIS2_PLACEMENT_3D ( 'NONE', #12811, #97, #15470 ) ;
#3585=VECTOR ( 'NONE', #6738, 1000.000000000000000 ) ;
#3591=ORIENTED_EDGE ( 'NONE', *, *, #1549, .T. ) ;
#3594=CARTESIAN_POINT ( 'NONE',  ( 21.00000000000000000, 8.000000000000000000, -31.00000000000003908 ) ) ;
#3614=CIRCLE ( 'NONE', #8274, 10.00000000000000178 ) ;
#3616=DIRECTION ( 'NONE',  ( 0.000000000000000000, 0.000000000000000000, 1.000000000000000000 ) ) ;
#3622=AXIS2_PLACEMENT_3D ( 'NONE', #5036, #5124, #7867 ) ;
#3639=EDGE_LOOP ( 'NONE', ( #15500, #15284, #10446, #9907 ) ) ;
#3644=CARTESIAN_POINT ( 'NONE',  ( 0.000000000000000000, -3.000000000000000000, 35.00000000000000711 ) ) ;
#3646=DIRECTION ( 'NONE',  ( -0.000000000000000000, -1.000000000000000000, 0.000000000000000000 ) ) ;
#3648=VECTOR ( 'NONE', #3511, 1000.000000000000000 ) ;
#3669=VECTOR ( 'NONE', #14100, 1000.000000000000000 ) ;
#3685=CIRCLE ( 'NONE', #13844, 10.00000000000000178 ) ;
#3703=( NAMED_UNIT ( * ) PLANE_ANGLE_UNIT ( ) SI_UNIT ( $, .RADIAN. ) );
#3714=EDGE_LOOP ( 'NONE', ( #282, #10853 ) ) ;
#3719=LINE ( 'NONE', #7561, #6678 ) ;
#3725=AXIS2_PLACEMENT_3D ( 'NONE', #14139, #12841, #11542 ) ;
#3732=EDGE_CURVE ( 'NONE', #9656, #4133, #13570, .T. ) ;
#3744=DIRECTION ( 'NONE',  ( -1.000000000000000000, -0.000000000000000000, -0.000000000000000000 ) ) ;
#3754=CIRCLE ( 'NONE', #10331, 5.000000000000000888 ) ;
#3767=DIRECTION ( 'NONE',  ( 0.000000000000000000, 1.000000000000000000, 0.000000000000000000 ) ) ;
#3780=DIRECTION ( 'NONE',  ( 0.000000000000000000, 0.000000000000000000, 1.000000000000000000 ) ) ;
#3782=EDGE_LOOP ( 'NONE', ( #15943, #8785, #15454, #12833 ) ) ;
#3787=DIRECTION ( 'NONE',  ( -0.000000000000000000, -1.000000000000000000, -0.000000000000000000 ) ) ;
#3799=DIRECTION ( 'NONE',  ( 1.000000000000000000, -0.000000000000000000, 0.000000000000000000 ) ) ;
#3804=ORIENTED_EDGE ( 'NONE', *, *, #5179, .T. ) ;
#3808=ORIENTED_EDGE ( 'NONE', *, *, #12141, .F. ) ;
#3818=CYLINDRICAL_SURFACE ( 'NONE', #3725, 35.00000000000000711 ) ;
#3819=ORIENTED_EDGE ( 'NONE', *, *, #9144, .F. ) ;
#3828=PRODUCT_DEFINITION_SHAPE ( 'NONE', 'NONE',  #6603 ) ;
#3845=EDGE_CURVE ( 'NONE', #14012, #12430, #6910, .T. ) ;
#3854=CARTESIAN_POINT ( 'NONE',  ( -31.00000000000003553, 19.00000000000000000, -21.00000000000000000 ) ) ;
#3862=FACE_OUTER_BOUND ( 'NONE', #10803, .T. ) ;
#3868=FACE_OUTER_BOUND ( 'NONE', #11774, .T. ) ;
#3875=DIRECTION ( 'NONE',  ( 0.000000000000000000, 0.000000000000000000, 1.000000000000000000 ) ) ;
#3883=ORIENTED_EDGE ( 'NONE', *, *, #10148, .T. ) ;
#3893=CIRCLE ( 'NONE', #3068, 3.299999999999997158 ) ;
#3909=DIRECTION ( 'NONE',  ( 0.000000000000000000, 1.000000000000000000, -0.000000000000000000 ) ) ;
#3920=CYLINDRICAL_SURFACE ( 'NONE', #4712, 3.300000000000000711 ) ;
#3925=ORIENTED_EDGE ( 'NONE', *, *, #16935, .T. ) ;
#3931=DIRECTION ( 'NONE',  ( -1.000000000000000000, -0.000000000000000000, -0.000000000000000000 ) ) ;
#3937=VECTOR ( 'NONE', #7136, 1000.000000000000000 ) ;
#3939=CARTESIAN_POINT ( 'NONE',  ( -35.00000000000000000, 8.000000000000000000, 20.99999999999999289 ) ) ;
#3945=DIRECTION ( 'NONE',  ( -0.000000000000000000, -1.000000000000000000, -0.000000000000000000 ) ) ;
#3969=DIRECTION ( 'NONE',  ( 0.000000000000000000, 0.000000000000000000, -1.000000000000000000 ) ) ;
#3978=AXIS2_PLACEMENT_3D ( 'NONE', #16733, #4893, #9021 ) ;
#3986=FACE_OUTER_BOUND ( 'NONE', #16369, .T. ) ;
#3987=VERTEX_POINT ( 'NONE', #1052 ) ;
#4000=ORIENTED_EDGE ( 'NONE', *, *, #1942, .F. ) ;
#4003=EDGE_CURVE ( 'NONE', #2412, #2603, #3719, .T. ) ;
#4004=CARTESIAN_POINT ( 'NONE',  ( -20.99999999999999645, 8.000000000000000000, -35.00000000000000711 ) ) ;
#4008=LINE ( 'NONE', #4936, #10516 ) ;
#4023=LINE ( 'NONE', #12213, #10770 ) ;
#4030=DIRECTION ( 'NONE',  ( -0.000000000000000000, -0.000000000000000000, 1.000000000000000000 ) ) ;
#4032=CARTESIAN_POINT ( 'NONE',  ( -31.00000000000000000, 11.00000000000000000, 25.99999999999999645 ) ) ;
#4044=CARTESIAN_POINT ( 'NONE',  ( 31.00000000000000000, 19.00000000000000000, -31.00000000000000355 ) ) ;
#4047=CARTESIAN_POINT ( 'NONE',  ( 26.00000000000000000, 19.00000000000000000, 40.00000000000001421 ) ) ;
#4055=DIRECTION ( 'NONE',  ( -0.000000000000000000, -1.000000000000000000, -0.000000000000000000 ) ) ;
#4056=ADVANCED_FACE ( 'NONE', ( #12819 ), #15482, .T. ) ;
#4069=CIRCLE ( 'NONE', #789, 9.999999999999998224 ) ;
#4070=CARTESIAN_POINT ( 'NONE',  ( 31.00000000000003553, 8.000000000000000000, 20.99999999999999289 ) ) ;
#4072=LINE ( 'NONE', #8269, #927 ) ;
#4084=ADVANCED_FACE ( 'NONE', ( #16074 ), #4320, .T. ) ;
#4100=LINE ( 'NONE', #1350, #9635 ) ;
#4102=ORIENTED_EDGE ( 'NONE', *, *, #5406, .T. ) ;
#4122=CARTESIAN_POINT ( 'NONE',  ( 31.81980515339464333, 0.000000000000000000, 31.81980515339463622 ) ) ;
#4133=VERTEX_POINT ( 'NONE', #8084 ) ;
#4153=EDGE_CURVE ( 'NONE', #12229, #10460, #14613, .T. ) ;
#4156=EDGE_CURVE ( 'NONE', #5761, #6577, #3163, .T. ) ;
#4174=ADVANCED_FACE ( 'NONE', ( #7041 ), #4226, .T. ) ;
#4181=ORIENTED_EDGE ( 'NONE', *, *, #2457, .F. ) ;
#4184=LINE ( 'NONE', #1607, #13043 ) ;
#4198=DIRECTION ( 'NONE',  ( -0.000000000000000000, -1.000000000000000000, -0.000000000000000000 ) ) ;
#4201=STYLED_ITEM ( 'NONE', ( #14694 ), #14480 ) ;
#4211=AXIS2_PLACEMENT_3D ( 'NONE', #14659, #2968, #14824 ) ;
#4214=CARTESIAN_POINT ( 'NONE',  ( -40.00000000000000000, 19.00000000000000000, -26.00000000000000355 ) ) ;
#4225=CIRCLE ( 'NONE', #2846, 3.299999999999997158 ) ;
#4226=CYLINDRICAL_SURFACE ( 'NONE', #679, 4.999999999999997335 ) ;
#4235=PLANE ( 'NONE',  #5237 ) ;
#4239=VERTEX_POINT ( 'NONE', #4811 ) ;
#4255=EDGE_CURVE ( 'NONE', #4694, #15712, #12738, .T. ) ;
#4260=VECTOR ( 'NONE', #11314, 1000.000000000000000 ) ;
#4270=DIRECTION ( 'NONE',  ( -1.000000000000000000, 0.000000000000000000, -0.000000000000000000 ) ) ;
#4282=CARTESIAN_POINT ( 'NONE',  ( -31.00000000000003553, 11.00000000000000000, -26.00000000000000355 ) ) ;
#4300=VECTOR ( 'NONE', #8168, 1000.000000000000000 ) ;
#4305=ORIENTED_EDGE ( 'NONE', *, *, #14674, .T. ) ;
#4318=VERTEX_POINT ( 'NONE', #3198 ) ;
#4319=ORIENTED_EDGE ( 'NONE', *, *, #6846, .F. ) ;
#4320=PLANE ( 'NONE',  #13579 ) ;
#4329=CARTESIAN_POINT ( 'NONE',  ( 35.00000000000000711, 0.000000000000000000, -35.00000000000000711 ) ) ;
#4331=EDGE_LOOP ( 'NONE', ( #2314, #8097, #16618, #6428 ) ) ;
#4353=LINE ( 'NONE', #10784, #13701 ) ;
#4379=ORIENTED_EDGE ( 'NONE', *, *, #9100, .F. ) ;
#4380=EDGE_CURVE ( 'NONE', #16035, #742, #6172, .T. ) ;
#4386=LINE ( 'NONE', #12108, #5835 ) ;
#4387=CIRCLE ( 'NONE', #13978, 4.999999999999997335 ) ;
#4391=ORIENTED_EDGE ( 'NONE', *, *, #6533, .T. ) ;
#4397=ORIENTED_EDGE ( 'NONE', *, *, #15958, .F. ) ;
#4402=EDGE_CURVE ( 'NONE', #10404, #8973, #11368, .T. ) ;
#4406=ORIENTED_EDGE ( 'NONE', *, *, #1627, .F. ) ;
#4409=VECTOR ( 'NONE', #5171, 1000.000000000000000 ) ;
#4411=AXIS2_PLACEMENT_3D ( 'NONE', #11905, #5537, #4270 ) ;
#4412=DIRECTION ( 'NONE',  ( 0.000000000000000000, 0.000000000000000000, -1.000000000000000000 ) ) ;
#4422=VERTEX_POINT ( 'NONE', #14087 ) ;
#4423=ORIENTED_EDGE ( 'NONE', *, *, #7781, .T. ) ;
#4426=DIRECTION ( 'NONE',  ( -0.000000000000000000, -1.000000000000000000, -0.000000000000000000 ) ) ;
#4428=FACE_OUTER_BOUND ( 'NONE', #12678, .T. ) ;
#4435=ORIENTED_EDGE ( 'NONE', *, *, #14239, .F. ) ;
#4436=ORIENTED_EDGE ( 'NONE', *, *, #4003, .T. ) ;
#4438=LINE ( 'NONE', #15256, #14306 ) ;
#4439=ADVANCED_FACE ( 'NONE', ( #3862 ), #9101, .F. ) ;
#4464=EDGE_CURVE ( 'NONE', #5920, #11543, #8849, .T. ) ;
#4469=ADVANCED_FACE ( 'NONE', ( #8937, #14178 ), #7627, .T. ) ;
#4470=VECTOR ( 'NONE', #13960, 1000.000000000000000 ) ;
#4477=VERTEX_POINT ( 'NONE', #12021 ) ;
#4501=CARTESIAN_POINT ( 'NONE',  ( -39.99999999999999289, 0.000000000000000000, 34.99999999999997868 ) ) ;
#4502=ORIENTED_EDGE ( 'NONE', *, *, #5179, .F. ) ;
#4513=FACE_OUTER_BOUND ( 'NONE', #6047, .T. ) ;
#4514=LINE ( 'NONE', #398, #11463 ) ;
#4533=CARTESIAN_POINT ( 'NONE',  ( -31.00000000000003553, 19.00000000000000000, 25.99999999999999645 ) ) ;
#4534=ORIENTED_EDGE ( 'NONE', *, *, #5200, .F. ) ;
#4542=CARTESIAN_POINT ( 'NONE',  ( -39.99999999999999289, 8.000000000000000000, 34.99999999999997868 ) ) ;
#4543=CARTESIAN_POINT ( 'NONE',  ( 21.00000000000000000, 19.00000000000000000, -31.00000000000003908 ) ) ;
#4548=AXIS2_PLACEMENT_3D ( 'NONE', #4122, #13330, #14697 ) ;
#4549=EDGE_LOOP ( 'NONE', ( #10948, #9125, #11985, #6566 ) ) ;
#4579=CIRCLE ( 'NONE', #10068, 3.299999999999997158 ) ;
#4583=EDGE_CURVE ( 'NONE', #394, #16829, #5345, .T. ) ;
#4592=CARTESIAN_POINT ( 'NONE',  ( 40.00000000000000711, 11.00000000000000000, 34.99999999999997868 ) ) ;
#4595=CARTESIAN_POINT ( 'NONE',  ( -39.99999999999999289, 0.000000000000000000, -34.99999999999997868 ) ) ;
#4596=ORIENTED_EDGE ( 'NONE', *, *, #8365, .F. ) ;
#4599=CARTESIAN_POINT ( 'NONE',  ( -34.99999999999996447, 0.000000000000000000, 40.00000000000000711 ) ) ;
#4612=ORIENTED_EDGE ( 'NONE', *, *, #3207, .T. ) ;
#4615=DIRECTION ( 'NONE',  ( 0.000000000000000000, 1.000000000000000000, 0.000000000000000000 ) ) ;
#4622=VECTOR ( 'NONE', #6950, 1000.000000000000000 ) ;
#4637=EDGE_CURVE ( 'NONE', #6773, #742, #6684, .T. ) ;
#4643=ORIENTED_EDGE ( 'NONE', *, *, #1765, .T. ) ;
#4648=ORIENTED_EDGE ( 'NONE', *, *, #8109, .T. ) ;
#4652=VERTEX_POINT ( 'NONE', #1880 ) ;
#4655=AXIS2_PLACEMENT_3D ( 'NONE', #13312, #12596, #5903 ) ;
#4660=FACE_OUTER_BOUND ( 'NONE', #14218, .T. ) ;
#4674=ORIENTED_EDGE ( 'NONE', *, *, #1441, .T. ) ;
#4685=EDGE_CURVE ( 'NONE', #4809, #1870, #967, .T. ) ;
#4694=VERTEX_POINT ( 'NONE', #1956 ) ;
#4706=ORIENTED_EDGE ( 'NONE', *, *, #11748, .F. ) ;
#4708=LINE ( 'NONE', #5674, #14217 ) ;
#4712=AXIS2_PLACEMENT_3D ( 'NONE', #14060, #7520, #149 ) ;
#4716=ORIENTED_EDGE ( 'NONE', *, *, #1993, .T. ) ;
#4744=DIRECTION ( 'NONE',  ( 0.000000000000000000, 1.000000000000000000, -0.000000000000000000 ) ) ;
#4756=CIRCLE ( 'NONE', #14086, 4.999999999999997335 ) ;
#4765=ORIENTED_EDGE ( 'NONE', *, *, #2784, .F. ) ;
#4768=CARTESIAN_POINT ( 'NONE',  ( -34.99999999999996447, 0.000000000000000000, 40.00000000000000711 ) ) ;
#4807=CARTESIAN_POINT ( 'NONE',  ( 35.00000000000000711, 8.000000000000000000, 20.99999999999999289 ) ) ;
#4809=VERTEX_POINT ( 'NONE', #2295 ) ;
#4811=CARTESIAN_POINT ( 'NONE',  ( 31.00000000000003553, 19.00000000000000000, 20.99999999999999289 ) ) ;
#4817=CARTESIAN_POINT ( 'NONE',  ( -31.81980515339462912, 8.000000000000000000, -28.51980515339464972 ) ) ;
#4821=DIRECTION ( 'NONE',  ( -0.000000000000000000, -1.000000000000000000, -0.000000000000000000 ) ) ;
#4822=VERTEX_POINT ( 'NONE', #12859 ) ;
#4834=CYLINDRICAL_SURFACE ( 'NONE', #1435, 4.999999999999997335 ) ;
#4835=CARTESIAN_POINT ( 'NONE',  ( -39.99999999999999289, 11.00000000000000000, -26.00000000000000355 ) ) ;
#4853=VERTEX_POINT ( 'NONE', #16796 ) ;
#4866=CARTESIAN_POINT ( 'NONE',  ( -35.00000000000000000, 8.000000000000000000, -21.00000000000000000 ) ) ;
#4869=CYLINDRICAL_SURFACE ( 'NONE', #7336, 4.999999999999997335 ) ;
#4876=EDGE_CURVE ( 'NONE', #9661, #12229, #8098, .T. ) ;
#4885=ORIENTED_EDGE ( 'NONE', *, *, #8653, .T. ) ;
#4893=DIRECTION ( 'NONE',  ( -0.000000000000000000, -1.000000000000000000, -0.000000000000000000 ) ) ;
#4896=LINE ( 'NONE', #14578, #4949 ) ;
#4897=VERTEX_POINT ( 'NONE', #15435 ) ;
#4902=LINE ( 'NONE', #2239, #10860 ) ;
#4910=PRODUCT ( 'Servo-Head', 'Servo-Head', '', ( #15300 ) ) ;
#4920=FACE_OUTER_BOUND ( 'NONE', #5568, .T. ) ;
#4922=DIRECTION ( 'NONE',  ( 0.000000000000000000, -1.000000000000000000, 0.000000000000000000 ) ) ;
#4924=VERTEX_POINT ( 'NONE', #11916 ) ;
#4926=ORIENTED_EDGE ( 'NONE', *, *, #15504, .F. ) ;
#4935=EDGE_LOOP ( 'NONE', ( #8859, #14753, #4319, #6458, #11809, #11446, #4926, #3819 ) ) ;
#4936=CARTESIAN_POINT ( 'NONE',  ( 31.81980515339464333, 8.000000000000000000, 28.51980515339463906 ) ) ;
#4941=VECTOR ( 'NONE', #2626, 1000.000000000000000 ) ;
#4949=VECTOR ( 'NONE', #14091, 1000.000000000000000 ) ;
#4952=EDGE_CURVE ( 'NONE', #10385, #7889, #4184, .T. ) ;
#4963=LINE ( 'NONE', #4807, #10622 ) ;
#4974=CARTESIAN_POINT ( 'NONE',  ( -39.99999999999999289, 8.000000000000000000, -34.99999999999997868 ) ) ;
#4987=ORIENTED_EDGE ( 'NONE', *, *, #8897, .F. ) ;
#4992=EDGE_CURVE ( 'NONE', #7414, #14012, #6173, .T. ) ;
#5012=EDGE_LOOP ( 'NONE', ( #4397, #13768, #15049, #14951 ) ) ;
#5036=CARTESIAN_POINT ( 'NONE',  ( -20.99999999999999645, 19.00000000000000000, 35.00000000000001421 ) ) ;
#5057=DIRECTION ( 'NONE',  ( -0.000000000000000000, -1.000000000000000000, -0.000000000000000000 ) ) ;
#5059=AXIS2_PLACEMENT_3D ( 'NONE', #4044, #7974, #13233 ) ;
#5064=DIRECTION ( 'NONE',  ( -0.000000000000000000, -1.000000000000000000, -0.000000000000000000 ) ) ;
#5071=VECTOR ( 'NONE', #13554, 1000.000000000000000 ) ;
#5083=CARTESIAN_POINT ( 'NONE',  ( 26.00000000000000000, 19.00000000000000000, 31.00000000000003197 ) ) ;
#5101=ORIENTED_EDGE ( 'NONE', *, *, #15624, .F. ) ;
#5107=CARTESIAN_POINT ( 'NONE',  ( -20.99999999999999645, 8.000000000000000000, 35.00000000000001421 ) ) ;
#5120=ORIENTED_EDGE ( 'NONE', *, *, #8266, .T. ) ;
#5123=AXIS2_PLACEMENT_3D ( 'NONE', #10232, #10401, #3969 ) ;
#5124=DIRECTION ( 'NONE',  ( 1.000000000000000000, -0.000000000000000000, 0.000000000000000000 ) ) ;
#5128=VECTOR ( 'NONE', #10558, 1000.000000000000000 ) ;
#5132=DIRECTION ( 'NONE',  ( -0.000000000000000000, -1.000000000000000000, -0.000000000000000000 ) ) ;
#5145=ORIENTED_EDGE ( 'NONE', *, *, #8083, .T. ) ;
#5171=DIRECTION ( 'NONE',  ( 0.000000000000000000, 0.000000000000000000, 1.000000000000000000 ) ) ;
#5172=ORIENTED_EDGE ( 'NONE', *, *, #11498, .F. ) ;
#5179=EDGE_CURVE ( 'NONE', #10304, #9656, #13794, .T. ) ;
#5181=EDGE_CURVE ( 'NONE', #16882, #7581, #5973, .T. ) ;
#5191=CARTESIAN_POINT ( 'NONE',  ( -31.81980515339462912, 11.00000000000000000, -28.51980515339464972 ) ) ;
#5200=EDGE_CURVE ( 'NONE', #1954, #9661, #9594, .T. ) ;
#5210=CARTESIAN_POINT ( 'NONE',  ( -35.00000000000000000, 19.00000000000000000, 20.99999999999999289 ) ) ;
#5225=ORIENTED_EDGE ( 'NONE', *, *, #695, .T. ) ;
#5228=FACE_OUTER_BOUND ( 'NONE', #12131, .T. ) ;
#5237=AXIS2_PLACEMENT_3D ( 'NONE', #10845, #14534, #370 ) ;
#5262=CARTESIAN_POINT ( 'NONE',  ( 21.00000000000000000, 19.00000000000000000, -31.00000000000003908 ) ) ;
#5268=VECTOR ( 'NONE', #12444, 1000.000000000000000 ) ;
#5270=ADVANCED_FACE ( 'NONE', ( #8980, #10353 ), #14293, .T. ) ;
#5272=EDGE_CURVE ( 'NONE', #7648, #2603, #15511, .T. ) ;
#5284=EDGE_CURVE ( 'NONE', #6577, #1719, #2356, .T. ) ;
#5291=VECTOR ( 'NONE', #3390, 1000.000000000000000 ) ;
#5295=AXIS2_PLACEMENT_3D ( 'NONE', #7673, #12927, #313 ) ;
#5317=CARTESIAN_POINT ( 'NONE',  ( 34.99999999999997868, 11.00000000000000000, 40.00000000000000711 ) ) ;
#5324=ORIENTED_EDGE ( 'NONE', *, *, #566, .T. ) ;
#5325=LINE ( 'NONE', #4047, #3669 ) ;
#5327=CARTESIAN_POINT ( 'NONE',  ( 31.00000000000000000, 8.000000000000000000, -21.00000000000000355 ) ) ;
#5345=CIRCLE ( 'NONE', #9469, 5.000000000000000888 ) ;
#5347=ADVANCED_FACE ( 'NONE', ( #8902 ), #3818, .T. ) ;
#5384=PLANE ( 'NONE',  #3107 ) ;
#5387=ORIENTED_EDGE ( 'NONE', *, *, #14777, .T. ) ;
#5396=DIRECTION ( 'NONE',  ( 0.000000000000000000, 1.000000000000000000, 0.000000000000000000 ) ) ;
#5402=FACE_OUTER_BOUND ( 'NONE', #830, .T. ) ;
#5406=EDGE_CURVE ( 'NONE', #6577, #11977, #15916, .T. ) ;
#5441=ORIENTED_EDGE ( 'NONE', *, *, #2986, .T. ) ;
#5446=PLANE ( 'NONE',  #7484 ) ;
#5464=VECTOR ( 'NONE', #3117, 1000.000000000000000 ) ;
#5478=DIRECTION ( 'NONE',  ( -0.000000000000000000, -1.000000000000000000, -0.000000000000000000 ) ) ;
#5485=ORIENTED_EDGE ( 'NONE', *, *, #9975, .T. ) ;
#5505=ORIENTED_EDGE ( 'NONE', *, *, #4402, .T. ) ;
#5506=CARTESIAN_POINT ( 'NONE',  ( 0.000000000000000000, 8.000000000000000000, -18.50000000000000000 ) ) ;
#5511=ORIENTED_EDGE ( 'NONE', *, *, #4952, .F. ) ;
#5536=EDGE_CURVE ( 'NONE', #11631, #2412, #16071, .T. ) ;
#5537=DIRECTION ( 'NONE',  ( 0.000000000000000000, 0.000000000000000000, -1.000000000000000000 ) ) ;
#5540=PLANE ( 'NONE',  #10599 ) ;
#5568=EDGE_LOOP ( 'NONE', ( #11750, #13327, #5929, #4423 ) ) ;
#5598=EDGE_CURVE ( 'NONE', #2603, #7648, #15250, .T. ) ;
#5602=VERTEX_POINT ( 'NONE', #3009 ) ;
#5625=DIRECTION ( 'NONE',  ( -0.000000000000000000, -1.000000000000000000, -0.000000000000000000 ) ) ;
#5658=DIRECTION ( 'NONE',  ( 0.000000000000000000, 0.000000000000000000, -1.000000000000000000 ) ) ;
#5665=( NAMED_UNIT ( * ) PLANE_ANGLE_UNIT ( ) SI_UNIT ( $, .RADIAN. ) );
#5674=CARTESIAN_POINT ( 'NONE',  ( 34.99999999999997868, 11.00000000000000000, -40.00000000000000711 ) ) ;
#5690=LINE ( 'NONE', #10072, #9147 ) ;
#5693=AXIS2_PLACEMENT_3D ( 'NONE', #13999, #469, #5696 ) ;
#5696=DIRECTION ( 'NONE',  ( 0.000000000000000000, 0.000000000000000000, -1.000000000000000000 ) ) ;
#5703=ORIENTED_EDGE ( 'NONE', *, *, #5536, .F. ) ;
#5711=CARTESIAN_POINT ( 'NONE',  ( -20.99999999999999645, 19.00000000000000000, -35.00000000000000711 ) ) ;
#5731=DIRECTION ( 'NONE',  ( 0.000000000000000000, 0.000000000000000000, 1.000000000000000000 ) ) ;
#5735=FACE_OUTER_BOUND ( 'NONE', #8222, .T. ) ;
#5761=VERTEX_POINT ( 'NONE', #14950 ) ;
#5764=EDGE_LOOP ( 'NONE', ( #5485, #1396, #7652, #11654 ) ) ;
#5767=FACE_BOUND ( 'NONE', #538, .T. ) ;
#5780=ORIENTED_EDGE ( 'NONE', *, *, #2381, .T. ) ;
#5790=EDGE_CURVE ( 'NONE', #4477, #3987, #12254, .T. ) ;
#5792=DIRECTION ( 'NONE',  ( 0.000000000000000000, 0.000000000000000000, 1.000000000000000000 ) ) ;
#5794=CARTESIAN_POINT ( 'NONE',  ( 26.00000000000000000, 19.00000000000000000, 40.00000000000001421 ) ) ;
#5795=DIRECTION ( 'NONE',  ( 1.000000000000000000, 0.000000000000000000, 0.000000000000000000 ) ) ;
#5806=FACE_OUTER_BOUND ( 'NONE', #2701, .T. ) ;
#5813=ORIENTED_EDGE ( 'NONE', *, *, #15958, .T. ) ;
#5824=VECTOR ( 'NONE', #8744, 1000.000000000000000 ) ;
#5835=VECTOR ( 'NONE', #9621, 1000.000000000000000 ) ;
#5837=DIRECTION ( 'NONE',  ( -0.000000000000000000, -0.000000000000000000, 1.000000000000000000 ) ) ;
#5845=ORIENTED_EDGE ( 'NONE', *, *, #6632, .T. ) ;
#5856=EDGE_LOOP ( 'NONE', ( #11115, #14790, #5225, #1845 ) ) ;
#5876=PLANE ( 'NONE',  #11339 ) ;
#5890=ORIENTED_EDGE ( 'NONE', *, *, #9670, .T. ) ;
#5899=DIRECTION ( 'NONE',  ( 0.000000000000000000, 0.000000000000000000, -1.000000000000000000 ) ) ;
#5901=CARTESIAN_POINT ( 'NONE',  ( 31.00000000000000000, 19.00000000000000000, -31.00000000000000355 ) ) ;
#5903=DIRECTION ( 'NONE',  ( 0.000000000000000000, 0.000000000000000000, 1.000000000000000000 ) ) ;
#5904=AXIS2_PLACEMENT_3D ( 'NONE', #13964, #910, #10099 ) ;
#5920=VERTEX_POINT ( 'NONE', #2466 ) ;
#5929=ORIENTED_EDGE ( 'NONE', *, *, #2784, .T. ) ;
#5934=CARTESIAN_POINT ( 'NONE',  ( 31.00000000000003908, 19.00000000000000000, -26.00000000000000355 ) ) ;
#5960=CARTESIAN_POINT ( 'NONE',  ( 34.99999999999997868, 0.000000000000000000, -40.00000000000000711 ) ) ;
#5973=LINE ( 'NONE', #11048, #15778 ) ;
#5977=EDGE_LOOP ( 'NONE', ( #2999, #15317, #3382, #12755 ) ) ;
#5986=CARTESIAN_POINT ( 'NONE',  ( 21.00000000000000000, 8.000000000000000000, 35.00000000000001421 ) ) ;
#5993=CARTESIAN_POINT ( 'NONE',  ( -31.81980515339462912, 11.00000000000000000, 31.81980515339465043 ) ) ;
#5994=VERTEX_POINT ( 'NONE', #3939 ) ;
#5997=PLANE ( 'NONE',  #16625 ) ;
#6008=ORIENTED_EDGE ( 'NONE', *, *, #7180, .F. ) ;
#6010=CARTESIAN_POINT ( 'NONE',  ( -40.00000000000000000, 19.00000000000000000, 25.99999999999999645 ) ) ;
#6033=CARTESIAN_POINT ( 'NONE',  ( -20.99999999999999645, 8.000000000000000000, 31.00000000000003197 ) ) ;
#6035=DIRECTION ( 'NONE',  ( -0.000000000000000000, -1.000000000000000000, -0.000000000000000000 ) ) ;
#6047=EDGE_LOOP ( 'NONE', ( #15814, #16227, #11550, #7320 ) ) ;
#6096=ORIENTED_EDGE ( 'NONE', *, *, #14332, .T. ) ;
#6104=AXIS2_PLACEMENT_3D ( 'NONE', #3071, #8305, #3167 ) ;
#6125=CARTESIAN_POINT ( 'NONE',  ( -31.81980515339462912, 8.000000000000000000, -35.11980515339465114 ) ) ;
#6131=CARTESIAN_POINT ( 'NONE',  ( -20.99999999999999645, 19.00000000000000000, 31.00000000000003197 ) ) ;
#6132=EDGE_CURVE ( 'NONE', #14475, #10621, #11142, .T. ) ;
#6144=LINE ( 'NONE', #4070, #15543 ) ;
#6151=CARTESIAN_POINT ( 'NONE',  ( 31.00000000000003553, 19.00000000000000000, 25.99999999999999645 ) ) ;
#6168=LINE ( 'NONE', #15620, #564 ) ;
#6169=PLANE ( 'NONE',  #1580 ) ;
#6171=ORIENTED_EDGE ( 'NONE', *, *, #6223, .F. ) ;
#6172=LINE ( 'NONE', #6415, #2307 ) ;
#6173=CIRCLE ( 'NONE', #11660, 4.999999999999997335 ) ;
#6179=CYLINDRICAL_SURFACE ( 'NONE', #1491, 3.299999999999997158 ) ;
#6204=ORIENTED_EDGE ( 'NONE', *, *, #1544, .F. ) ;
#6205=CARTESIAN_POINT ( 'NONE',  ( -31.00000000000000000, 19.00000000000000000, 30.99999999999999289 ) ) ;
#6223=EDGE_CURVE ( 'NONE', #13441, #10385, #3754, .T. ) ;
#6227=CIRCLE ( 'NONE', #8983, 3.299999999999997158 ) ;
#6250=EDGE_CURVE ( 'NONE', #4652, #7581, #4579, .T. ) ;
#6281=DIRECTION ( 'NONE',  ( 0.000000000000000000, 0.000000000000000000, 1.000000000000000000 ) ) ;
#6303=CARTESIAN_POINT ( 'NONE',  ( 0.000000000000000000, 0.000000000000000000, 0.000000000000000000 ) ) ;
#6359=ORIENTED_EDGE ( 'NONE', *, *, #10182, .T. ) ;
#6361=EDGE_CURVE ( 'NONE', #12007, #13963, #6144, .T. ) ;
#6367=DIRECTION ( 'NONE',  ( 0.000000000000000000, -1.000000000000000000, 0.000000000000000000 ) ) ;
#6392=ORIENTED_EDGE ( 'NONE', *, *, #6361, .F. ) ;
#6402=DIRECTION ( 'NONE',  ( -1.000000000000000000, 0.000000000000000000, -0.000000000000000000 ) ) ;
#6408=LINE ( 'NONE', #5210, #10316 ) ;
#6415=CARTESIAN_POINT ( 'NONE',  ( 21.00000000000000000, 19.00000000000000000, 31.00000000000006395 ) ) ;
#6418=EDGE_CURVE ( 'NONE', #4822, #4318, #7514, .T. ) ;
#6422=LINE ( 'NONE', #4974, #10759 ) ;
#6423=CARTESIAN_POINT ( 'NONE',  ( -20.99999999999999645, 19.00000000000000000, -35.00000000000000711 ) ) ;
#6428=ORIENTED_EDGE ( 'NONE', *, *, #6976, .F. ) ;
#6430=VECTOR ( 'NONE', #7251, 1000.000000000000000 ) ;
#6454=ORIENTED_EDGE ( 'NONE', *, *, #7924, .T. ) ;
#6455=AXIS2_PLACEMENT_3D ( 'NONE', #10050, #8680, #7365 ) ;
#6457=CARTESIAN_POINT ( 'NONE',  ( -39.99999999999999289, 11.00000000000000000, 25.99999999999999645 ) ) ;
#6458=ORIENTED_EDGE ( 'NONE', *, *, #3845, .F. ) ;
#6464=ORIENTED_EDGE ( 'NONE', *, *, #2291, .F. ) ;
#6469=ORIENTED_EDGE ( 'NONE', *, *, #259, .T. ) ;
#6481=AXIS2_PLACEMENT_3D ( 'NONE', #6205, #16612, #6281 ) ;
#6500=DIRECTION ( 'NONE',  ( 0.000000000000000000, 0.000000000000000000, -1.000000000000000000 ) ) ;
#6503=SHAPE_REPRESENTATION_RELATIONSHIP ( 'NONE' , 'NONE' ,  #11211, #2183 ) ;
#6504=CIRCLE ( 'NONE', #13941, 4.999999999999997335 ) ;
#6505=CYLINDRICAL_SURFACE ( 'NONE', #9942, 3.299999999999997158 ) ;
#6533=EDGE_CURVE ( 'NONE', #4318, #12218, #13091, .T. ) ;
#6551=ORIENTED_EDGE ( 'NONE', *, *, #8705, .F. ) ;
#6566=ORIENTED_EDGE ( 'NONE', *, *, #4402, .F. ) ;
#6577=VERTEX_POINT ( 'NONE', #3372 ) ;
#6582=CARTESIAN_POINT ( 'NONE',  ( -31.00000000000000000, 19.00000000000000000, -31.00000000000000000 ) ) ;
#6586=CARTESIAN_POINT ( 'NONE',  ( 31.00000000000000000, 11.00000000000000000, -31.00000000000000355 ) ) ;
#6588=EDGE_LOOP ( 'NONE', ( #4596, #16232, #10639, #10044, #16862, #6464, #4612, #11028 ) ) ;
#6591=VECTOR ( 'NONE', #11545, 1000.000000000000000 ) ;
#6592=EDGE_CURVE ( 'NONE', #16870, #2442, #8702, .T. ) ;
#6597=CARTESIAN_POINT ( 'NONE',  ( 35.00000000000000711, 0.000000000000000000, 35.00000000000000711 ) ) ;
#6603=PRODUCT_DEFINITION ( 'UNKNOWN', '', #11646, #10722 ) ;
#6604=ORIENTED_EDGE ( 'NONE', *, *, #7944, .T. ) ;
#6605=ORIENTED_EDGE ( 'NONE', *, *, #2752, .F. ) ;
#6610=ORIENTED_EDGE ( 'NONE', *, *, #1942, .T. ) ;
#6621=ORIENTED_EDGE ( 'NONE', *, *, #16093, .T. ) ;
#6632=EDGE_CURVE ( 'NONE', #15841, #10304, #4902, .T. ) ;
#6653=VECTOR ( 'NONE', #1581, 1000.000000000000000 ) ;
#6658=AXIS2_PLACEMENT_3D ( 'NONE', #11138, #16538, #915 ) ;
#6661=EDGE_CURVE ( 'NONE', #14614, #6773, #10152, .T. ) ;
#6673=EDGE_LOOP ( 'NONE', ( #7900, #8761, #869, #3591 ) ) ;
#6678=VECTOR ( 'NONE', #14359, 1000.000000000000000 ) ;
#6684=LINE ( 'NONE', #5986, #4260 ) ;
#6698=ORIENTED_EDGE ( 'NONE', *, *, #8456, .T. ) ;
#6713=LINE ( 'NONE', #13255, #9450 ) ;
#6726=CARTESIAN_POINT ( 'NONE',  ( -20.99999999999999645, 19.00000000000000000, 35.00000000000001421 ) ) ;
#6738=DIRECTION ( 'NONE',  ( -0.000000000000000000, -1.000000000000000000, -0.000000000000000000 ) ) ;
#6752=VERTEX_POINT ( 'NONE', #13072 ) ;
#6764=ADVANCED_FACE ( 'NONE', ( #5228 ), #9284, .F. ) ;
#6773=VERTEX_POINT ( 'NONE', #15559 ) ;
#6790=VERTEX_POINT ( 'NONE', #5327 ) ;
#6795=DIRECTION ( 'NONE',  ( 0.000000000000000000, -1.000000000000000000, 0.000000000000000000 ) ) ;
#6796=CIRCLE ( 'NONE', #1313, 35.00000000000000711 ) ;
#6797=CARTESIAN_POINT ( 'NONE',  ( -31.00000000000000000, 19.00000000000000000, -31.00000000000000000 ) ) ;
#6802=ORIENTED_EDGE ( 'NONE', *, *, #7180, .T. ) ;
#6809=ORIENTED_EDGE ( 'NONE', *, *, #7489, .F. ) ;
#6839=ORIENTED_EDGE ( 'NONE', *, *, #12765, .T. ) ;
#6846=EDGE_CURVE ( 'NONE', #12430, #2722, #10903, .T. ) ;
#6885=ORIENTED_EDGE ( 'NONE', *, *, #13083, .T. ) ;
#6895=ORIENTED_EDGE ( 'NONE', *, *, #9937, .F. ) ;
#6902=CARTESIAN_POINT ( 'NONE',  ( -26.00000000000000355, 11.00000000000000000, 31.00000000000003553 ) ) ;
#6904=CARTESIAN_POINT ( 'NONE',  ( -31.81980515339462912, 8.000000000000000000, 35.11980515339465825 ) ) ;
#6909=LINE ( 'NONE', #15155, #1164 ) ;
#6910=LINE ( 'NONE', #4599, #10538 ) ;
#6917=VECTOR ( 'NONE', #16191, 1000.000000000000000 ) ;
#6926=DIRECTION ( 'NONE',  ( -0.000000000000000000, -1.000000000000000000, -0.000000000000000000 ) ) ;
#6934=DIRECTION ( 'NONE',  ( 0.000000000000000000, -1.000000000000000000, 0.000000000000000000 ) ) ;
#6939=CARTESIAN_POINT ( 'NONE',  ( 26.00000000000000355, 11.00000000000000000, -40.00000000000000711 ) ) ;
#6940=( LENGTH_UNIT ( ) NAMED_UNIT ( * ) SI_UNIT ( .MILLI., .METRE. ) );
#6941=AXIS2_PLACEMENT_3D ( 'NONE', #9048, #16936, #10171 ) ;
#6944=VECTOR ( 'NONE', #734, 1000.000000000000000 ) ;
#6945=CARTESIAN_POINT ( 'NONE',  ( -31.81980515339462912, 8.000000000000000000, -31.81980515339465043 ) ) ;
#6950=DIRECTION ( 'NONE',  ( -0.000000000000000000, -1.000000000000000000, -0.000000000000000000 ) ) ;
#6960=VECTOR ( 'NONE', #13517, 1000.000000000000000 ) ;
#6966=ORIENTED_EDGE ( 'NONE', *, *, #5598, .F. ) ;
#6967=CARTESIAN_POINT ( 'NONE',  ( -26.00000000000000000, 11.00000000000000000, -40.00000000000000711 ) ) ;
#6976=EDGE_CURVE ( 'NONE', #11526, #11059, #3014, .T. ) ;
#6985=DIRECTION ( 'NONE',  ( -0.000000000000000000, -1.000000000000000000, -0.000000000000000000 ) ) ;
#6988=EDGE_LOOP ( 'NONE', ( #9373, #1616 ) ) ;
#6997=ADVANCED_FACE ( 'NONE', ( #9367 ), #14608, .F. ) ;
#6998=CARTESIAN_POINT ( 'NONE',  ( 26.00000000000000000, 19.00000000000000000, 40.00000000000001421 ) ) ;
#7005=VERTEX_POINT ( 'NONE', #16478 ) ;
#7006=VERTEX_POINT ( 'NONE', #3523 ) ;
#7009=CARTESIAN_POINT ( 'NONE',  ( 35.00000000000000711, 8.000000000000000000, 20.99999999999999289 ) ) ;
#7036=CARTESIAN_POINT ( 'NONE',  ( 0.000000000000000000, -3.000000000000000000, 35.00000000000000711 ) ) ;
#7041=FACE_OUTER_BOUND ( 'NONE', #7618, .T. ) ;
#7042=ORIENTED_EDGE ( 'NONE', *, *, #16609, .F. ) ;
#7054=ORIENTED_EDGE ( 'NONE', *, *, #4153, .T. ) ;
#7065=CARTESIAN_POINT ( 'NONE',  ( -39.99999999999999289, 11.00000000000000000, -34.99999999999997868 ) ) ;
#7088=PLANE ( 'NONE',  #10505 ) ;
#7092=ADVANCED_FACE ( 'NONE', ( #7288 ), #5997, .T. ) ;
#7093=VECTOR ( 'NONE', #13705, 1000.000000000000000 ) ;
#7102=VERTEX_POINT ( 'NONE', #16323 ) ;
#7118=AXIS2_PLACEMENT_3D ( 'NONE', #8294, #13379, #11998 ) ;
#7136=DIRECTION ( 'NONE',  ( -0.000000000000000000, -1.000000000000000000, -0.000000000000000000 ) ) ;
#7153=LINE ( 'NONE', #9682, #4470 ) ;
#7156=DIRECTION ( 'NONE',  ( 1.000000000000000000, 0.000000000000000000, 0.000000000000000000 ) ) ;
#7158=EDGE_LOOP ( 'NONE', ( #16674, #8023, #8733, #15161, #12742, #731 ) ) ;
#7166=VECTOR ( 'NONE', #11900, 1000.000000000000000 ) ;
#7174=LINE ( 'NONE', #4866, #8567 ) ;
#7176=CARTESIAN_POINT ( 'NONE',  ( -39.99999999999999289, 11.00000000000000000, -34.99999999999997868 ) ) ;
#7177=DIRECTION ( 'NONE',  ( 0.000000000000000000, 0.000000000000000000, -1.000000000000000000 ) ) ;
#7180=EDGE_CURVE ( 'NONE', #12818, #16324, #6408, .T. ) ;
#7200=ORIENTED_EDGE ( 'NONE', *, *, #596, .T. ) ;
#7202=ORIENTED_EDGE ( 'NONE', *, *, #13682, .T. ) ;
#7203=AXIS2_PLACEMENT_3D ( 'NONE', #8265, #6795, #10850 ) ;
#7213=LINE ( 'NONE', #16410, #5464 ) ;
#7221=EDGE_LOOP ( 'NONE', ( #9550, #474, #3331, #803 ) ) ;
#7224=VECTOR ( 'NONE', #10337, 1000.000000000000000 ) ;
#7236=CARTESIAN_POINT ( 'NONE',  ( 31.00000000000003553, 19.00000000000000000, 20.99999999999999289 ) ) ;
#7240=CARTESIAN_POINT ( 'NONE',  ( 31.81980515339464333, 11.00000000000000000, -35.11980515339463693 ) ) ;
#7241=DIRECTION ( 'NONE',  ( 0.000000000000000000, 0.000000000000000000, -1.000000000000000000 ) ) ;
#7251=DIRECTION ( 'NONE',  ( 1.000000000000000000, 0.000000000000000000, 0.000000000000000000 ) ) ;
#7262=DIRECTION ( 'NONE',  ( -0.000000000000000000, -1.000000000000000000, -0.000000000000000000 ) ) ;
#7288=FACE_OUTER_BOUND ( 'NONE', #12143, .T. ) ;
#7295=ORIENTED_EDGE ( 'NONE', *, *, #6418, .T. ) ;
#7310=DIRECTION ( 'NONE',  ( -0.000000000000000000, -1.000000000000000000, -0.000000000000000000 ) ) ;
#7316=AXIS2_PLACEMENT_3D ( 'NONE', #6797, #16254, #12054 ) ;
#7317=ORIENTED_EDGE ( 'NONE', *, *, #4153, .F. ) ;
#7320=ORIENTED_EDGE ( 'NONE', *, *, #5284, .T. ) ;
#7331=DIRECTION ( 'NONE',  ( -0.000000000000000000, -1.000000000000000000, -0.000000000000000000 ) ) ;
#7336=AXIS2_PLACEMENT_3D ( 'NONE', #930, #8823, #7177 ) ;
#7360=DIRECTION ( 'NONE',  ( 0.000000000000000000, 0.000000000000000000, -1.000000000000000000 ) ) ;
#7365=DIRECTION ( 'NONE',  ( 0.000000000000000000, 0.000000000000000000, -1.000000000000000000 ) ) ;
#7386=AXIS2_PLACEMENT_3D ( 'NONE', #2714, #2540, #12855 ) ;
#7390=ORIENTED_EDGE ( 'NONE', *, *, #8083, .F. ) ;
#7398=EDGE_LOOP ( 'NONE', ( #16889, #14841, #3494, #11524 ) ) ;
#7399=DIRECTION ( 'NONE',  ( 0.000000000000000000, 0.000000000000000000, -1.000000000000000000 ) ) ;
#7411=CIRCLE ( 'NONE', #2208, 4.999999999999997335 ) ;
#7414=VERTEX_POINT ( 'NONE', #590 ) ;
#7419=DIRECTION ( 'NONE',  ( 0.000000000000000000, -0.000000000000000000, 1.000000000000000000 ) ) ;
#7421=EDGE_LOOP ( 'NONE', ( #9748, #4534, #13217, #14171 ) ) ;
#7431=ORIENTED_EDGE ( 'NONE', *, *, #12150, .F. ) ;
#7460=CARTESIAN_POINT ( 'NONE',  ( 40.00000000000000711, 11.00000000000000000, 34.99999999999997868 ) ) ;
#7465=ORIENTED_EDGE ( 'NONE', *, *, #4156, .F. ) ;
#7484=AXIS2_PLACEMENT_3D ( 'NONE', #9404, #9243, #483 ) ;
#7489=EDGE_CURVE ( 'NONE', #1719, #15142, #16462, .T. ) ;
#7493=CARTESIAN_POINT ( 'NONE',  ( -31.00000000000000000, 19.00000000000000000, -31.00000000000000000 ) ) ;
#7501=DIRECTION ( 'NONE',  ( 0.000000000000000000, 1.000000000000000000, 0.000000000000000000 ) ) ;
#7514=LINE ( 'NONE', #12773, #14173 ) ;
#7517=EDGE_CURVE ( 'NONE', #1839, #11059, #185, .T. ) ;
#7520=DIRECTION ( 'NONE',  ( -0.000000000000000000, -1.000000000000000000, -0.000000000000000000 ) ) ;
#7549=CARTESIAN_POINT ( 'NONE',  ( 31.00000000000000000, 19.00000000000000000, 30.99999999999999289 ) ) ;
#7560=ORIENTED_EDGE ( 'NONE', *, *, #15747, .F. ) ;
#7561=CARTESIAN_POINT ( 'NONE',  ( 31.81980515339464333, 8.000000000000000000, 35.11980515339463693 ) ) ;
#7571=DIRECTION ( 'NONE',  ( 0.000000000000000000, 0.000000000000000000, 1.000000000000000000 ) ) ;
#7575=DIRECTION ( 'NONE',  ( 0.000000000000000000, 0.000000000000000000, -1.000000000000000000 ) ) ;
#7581=VERTEX_POINT ( 'NONE', #12852 ) ;
#7595=UNCERTAINTY_MEASURE_WITH_UNIT (LENGTH_MEASURE( 1.000000000000000082E-05 ), #11678, 'distance_accuracy_value', 'NONE');
#7603=FACE_OUTER_BOUND ( 'NONE', #7421, .T. ) ;
#7611=LINE ( 'NONE', #7778, #7709 ) ;
#7618=EDGE_LOOP ( 'NONE', ( #13271, #3547, #8865, #6454 ) ) ;
#7627=PLANE ( 'NONE',  #1795 ) ;
#7634=DIRECTION ( 'NONE',  ( -1.000000000000000000, -0.000000000000000000, -0.000000000000000000 ) ) ;
#7644=CIRCLE ( 'NONE', #15876, 10.00000000000000178 ) ;
#7648=VERTEX_POINT ( 'NONE', #1600 ) ;
#7652=ORIENTED_EDGE ( 'NONE', *, *, #13536, .F. ) ;
#7673=CARTESIAN_POINT ( 'NONE',  ( 0.000000000000000000, 0.000000000000000000, 0.000000000000000000 ) ) ;
#7692=PLANE ( 'NONE',  #8586 ) ;
#7703=ADVANCED_FACE ( 'NONE', ( #57 ), #5540, .F. ) ;
#7704=LINE ( 'NONE', #13054, #12436 ) ;
#7707=CARTESIAN_POINT ( 'NONE',  ( 31.81980515339464333, 8.000000000000000000, -31.81980515339463622 ) ) ;
#7709=VECTOR ( 'NONE', #15531, 1000.000000000000000 ) ;
#7710=CARTESIAN_POINT ( 'NONE',  ( 35.00000000000000711, 8.000000000000000000, -35.00000000000000711 ) ) ;
#7718=CARTESIAN_POINT ( 'NONE',  ( -31.00000000000000000, 11.00000000000000000, 30.99999999999999289 ) ) ;
#7768=CIRCLE ( 'NONE', #8615, 10.00000000000000178 ) ;
#7778=CARTESIAN_POINT ( 'NONE',  ( 31.00000000000003553, 19.00000000000000000, 25.99999999999999645 ) ) ;
#7780=DIRECTION ( 'NONE',  ( 0.000000000000000000, 0.000000000000000000, 1.000000000000000000 ) ) ;
#7781=EDGE_CURVE ( 'NONE', #2164, #8649, #2181, .T. ) ;
#7792=FACE_OUTER_BOUND ( 'NONE', #3528, .T. ) ;
#7793=CARTESIAN_POINT ( 'NONE',  ( -34.99999999999996447, 8.000000000000000000, -40.00000000000000711 ) ) ;
#7801=VECTOR ( 'NONE', #12803, 1000.000000000000000 ) ;
#7809=DIRECTION ( 'NONE',  ( 0.000000000000000000, 0.000000000000000000, -1.000000000000000000 ) ) ;
#7817=ORIENTED_EDGE ( 'NONE', *, *, #13293, .T. ) ;
#7827=VERTEX_POINT ( 'NONE', #12257 ) ;
#7830=CARTESIAN_POINT ( 'NONE',  ( 31.00000000000000000, 8.000000000000000000, 30.99999999999999289 ) ) ;
#7862=ORIENTED_EDGE ( 'NONE', *, *, #13902, .T. ) ;
#7863=AXIS2_PLACEMENT_3D ( 'NONE', #11456, #10173, #10854 ) ;
#7867=DIRECTION ( 'NONE',  ( 0.000000000000000000, 0.000000000000000000, -1.000000000000000000 ) ) ;
#7888=DIRECTION ( 'NONE',  ( -0.000000000000000000, -1.000000000000000000, -0.000000000000000000 ) ) ;
#7889=VERTEX_POINT ( 'NONE', #9921 ) ;
#7900=ORIENTED_EDGE ( 'NONE', *, *, #8266, .F. ) ;
#7924=EDGE_CURVE ( 'NONE', #10121, #10620, #8891, .T. ) ;
#7939=PLANE ( 'NONE',  #4411 ) ;
#7944=EDGE_CURVE ( 'NONE', #15084, #4897, #3488, .T. ) ;
#7965=DIRECTION ( 'NONE',  ( 0.000000000000000000, 0.000000000000000000, -1.000000000000000000 ) ) ;
#7966=ORIENTED_EDGE ( 'NONE', *, *, #350, .T. ) ;
#7974=DIRECTION ( 'NONE',  ( -0.000000000000000000, -1.000000000000000000, -0.000000000000000000 ) ) ;
#8003=LINE ( 'NONE', #11882, #6653 ) ;
#8004=EDGE_LOOP ( 'NONE', ( #15926, #6839, #12795, #9885 ) ) ;
#8015=ADVANCED_FACE ( 'NONE', ( #1239, #15652 ), #10264, .F. ) ;
#8023=ORIENTED_EDGE ( 'NONE', *, *, #14583, .T. ) ;
#8028=CARTESIAN_POINT ( 'NONE',  ( 0.000000000000000000, 19.00100000000000122, 0.000000000000000000 ) ) ;
#8031=CARTESIAN_POINT ( 'NONE',  ( -26.00000000000000000, 19.00000000000000000, 40.00000000000001421 ) ) ;
#8066=LINE ( 'NONE', #10990, #815 ) ;
#8083=EDGE_CURVE ( 'NONE', #3987, #4477, #15282, .T. ) ;
#8084=CARTESIAN_POINT ( 'NONE',  ( -26.00000000000000000, 11.00000000000000000, -31.00000000000003908 ) ) ;
#8097=ORIENTED_EDGE ( 'NONE', *, *, #9569, .T. ) ;
#8098=CIRCLE ( 'NONE', #14414, 4.999999999999997335 ) ;
#8099=FACE_OUTER_BOUND ( 'NONE', #11727, .T. ) ;
#8109=EDGE_CURVE ( 'NONE', #4239, #10479, #1402, .T. ) ;
#8115=CARTESIAN_POINT ( 'NONE',  ( -35.00000000000000000, 19.00000000000000000, -21.00000000000000000 ) ) ;
#8119=DIRECTION ( 'NONE',  ( -0.000000000000000000, -1.000000000000000000, -0.000000000000000000 ) ) ;
#8122=LINE ( 'NONE', #9249, #4941 ) ;
#8128=CARTESIAN_POINT ( 'NONE',  ( -31.00000000000000000, 11.00000000000000000, -31.00000000000000000 ) ) ;
#8137=CARTESIAN_POINT ( 'NONE',  ( -34.99999999999999289, 11.00000000000000000, -35.00000000000000711 ) ) ;
#8144=LINE ( 'NONE', #1794, #16963 ) ;
#8149=AXIS2_PLACEMENT_3D ( 'NONE', #6597, #11856, #15811 ) ;
#8157=CARTESIAN_POINT ( 'NONE',  ( -31.00000000000000000, 11.00000000000000000, -31.00000000000000000 ) ) ;
#8163=DIRECTION ( 'NONE',  ( -0.000000000000000000, -1.000000000000000000, -0.000000000000000000 ) ) ;
#8168=DIRECTION ( 'NONE',  ( -0.000000000000000000, 1.000000000000000000, -0.000000000000000000 ) ) ;
#8192=ORIENTED_EDGE ( 'NONE', *, *, #4380, .T. ) ;
#8206=DIRECTION ( 'NONE',  ( -0.000000000000000000, -1.000000000000000000, -0.000000000000000000 ) ) ;
#8219=ADVANCED_FACE ( 'NONE', ( #12144 ), #6169, .F. ) ;
#8222=EDGE_LOOP ( 'NONE', ( #15513, #12194, #10836, #6966 ) ) ;
#8237=ORIENTED_EDGE ( 'NONE', *, *, #16609, .T. ) ;
#8259=VECTOR ( 'NONE', #978, 1000.000000000000000 ) ;
#8265=CARTESIAN_POINT ( 'NONE',  ( 35.00000000000000711, 8.000000000000000000, -35.00000000000000711 ) ) ;
#8266=EDGE_CURVE ( 'NONE', #13963, #10961, #4963, .T. ) ;
#8269=CARTESIAN_POINT ( 'NONE',  ( -26.00000000000000000, 19.00000000000000000, -40.00000000000000711 ) ) ;
#8274=AXIS2_PLACEMENT_3D ( 'NONE', #7830, #2420, #11872 ) ;
#8285=DIRECTION ( 'NONE',  ( 0.000000000000000000, -1.000000000000000000, 0.000000000000000000 ) ) ;
#8294=CARTESIAN_POINT ( 'NONE',  ( -31.81980515339462912, 0.000000000000000000, 31.81980515339465043 ) ) ;
#8305=DIRECTION ( 'NONE',  ( 0.000000000000000000, 0.000000000000000000, 1.000000000000000000 ) ) ;
#8328=AXIS2_PLACEMENT_3D ( 'NONE', #8028, #8119, #13372 ) ;
#8345=DIRECTION ( 'NONE',  ( 0.000000000000000000, 0.000000000000000000, 1.000000000000000000 ) ) ;
#8351=ADVANCED_FACE ( 'NONE', ( #1756 ), #11331, .F. ) ;
#8358=CARTESIAN_POINT ( 'NONE',  ( 25.99999999999999645, 11.00000000000000000, 40.00000000000000711 ) ) ;
#8365=EDGE_CURVE ( 'NONE', #14475, #12430, #16172, .T. ) ;
#8370=PLANE ( 'NONE',  #645 ) ;
#8371=EDGE_LOOP ( 'NONE', ( #13432, #4436, #16455, #13103 ) ) ;
#8381=LINE ( 'NONE', #7065, #9680 ) ;
#8383=VECTOR ( 'NONE', #11149, 1000.000000000000000 ) ;
#8406=DIRECTION ( 'NONE',  ( 0.000000000000000000, 1.000000000000000000, 0.000000000000000000 ) ) ;
#8419=CARTESIAN_POINT ( 'NONE',  ( -34.99999999999999289, 11.00000000000000000, 35.00000000000000711 ) ) ;
#8434=DIRECTION ( 'NONE',  ( 0.000000000000000000, 0.000000000000000000, -1.000000000000000000 ) ) ;
#8444=PLANE ( 'NONE',  #7203 ) ;
#8456=EDGE_CURVE ( 'NONE', #16882, #12691, #6227, .T. ) ;
#8462=ADVANCED_FACE ( 'NONE', ( #7792 ), #13053, .F. ) ;
#8481=ORIENTED_EDGE ( 'NONE', *, *, #16059, .T. ) ;
#8495=DIRECTION ( 'NONE',  ( 0.000000000000000000, 0.000000000000000000, 1.000000000000000000 ) ) ;
#8501=DIRECTION ( 'NONE',  ( 0.000000000000000000, 0.000000000000000000, 1.000000000000000000 ) ) ;
#8519=VECTOR ( 'NONE', #3744, 1000.000000000000000 ) ;
#8530=ORIENTED_EDGE ( 'NONE', *, *, #15951, .F. ) ;
#8542=CARTESIAN_POINT ( 'NONE',  ( -20.99999999999999645, 8.000000000000000000, -31.00000000000003553 ) ) ;
#8567=VECTOR ( 'NONE', #9948, 1000.000000000000000 ) ;
#8572=CARTESIAN_POINT ( 'NONE',  ( -35.00000000000000000, 19.00000000000000000, -21.00000000000000000 ) ) ;
#8579=VECTOR ( 'NONE', #9588, 1000.000000000000000 ) ;
#8586=AXIS2_PLACEMENT_3D ( 'NONE', #2212, #12948, #6402 ) ;
#8598=ORIENTED_EDGE ( 'NONE', *, *, #8653, .F. ) ;
#8615=AXIS2_PLACEMENT_3D ( 'NONE', #13075, #15637, #3875 ) ;
#8616=DIRECTION ( 'NONE',  ( 0.000000000000000000, 0.000000000000000000, -1.000000000000000000 ) ) ;
#8618=ADVANCED_FACE ( 'NONE', ( #11066 ), #4869, .T. ) ;
#8627=EDGE_LOOP ( 'NONE', ( #9042, #11262 ) ) ;
#8634=DIRECTION ( 'NONE',  ( 0.000000000000000000, 1.000000000000000000, -0.000000000000000000 ) ) ;
#8635=AXIS2_PLACEMENT_3D ( 'NONE', #16840, #3799, #1222 ) ;
#8649=VERTEX_POINT ( 'NONE', #16308 ) ;
#8653=EDGE_CURVE ( 'NONE', #747, #7006, #9789, .T. ) ;
#8665=ORIENTED_EDGE ( 'NONE', *, *, #11405, .F. ) ;
#8671=CARTESIAN_POINT ( 'NONE',  ( -31.00000000000000000, 11.00000000000000000, 25.99999999999999645 ) ) ;
#8680=DIRECTION ( 'NONE',  ( -0.000000000000000000, -1.000000000000000000, -0.000000000000000000 ) ) ;
#8693=DIRECTION ( 'NONE',  ( 0.000000000000000000, 0.000000000000000000, 1.000000000000000000 ) ) ;
#8702=LINE ( 'NONE', #13938, #13057 ) ;
#8705=EDGE_CURVE ( 'NONE', #13859, #5920, #16451, .T. ) ;
#8719=DIRECTION ( 'NONE',  ( -0.000000000000000000, -1.000000000000000000, -0.000000000000000000 ) ) ;
#8726=CARTESIAN_POINT ( 'NONE',  ( 21.00000000000000000, 19.00000000000000000, -31.00000000000003908 ) ) ;
#8729=VERTEX_POINT ( 'NONE', #16881 ) ;
#8733=ORIENTED_EDGE ( 'NONE', *, *, #9100, .T. ) ;
#8744=DIRECTION ( 'NONE',  ( -0.000000000000000000, -1.000000000000000000, -0.000000000000000000 ) ) ;
#8761=ORIENTED_EDGE ( 'NONE', *, *, #3221, .F. ) ;
#8772=ADVANCED_FACE ( 'NONE', ( #13118 ), #9000, .F. ) ;
#8782=DIRECTION ( 'NONE',  ( -0.000000000000000000, -1.000000000000000000, 0.000000000000000000 ) ) ;
#8783=VERTEX_POINT ( 'NONE', #5191 ) ;
#8785=ORIENTED_EDGE ( 'NONE', *, *, #10182, .F. ) ;
#8797=CARTESIAN_POINT ( 'NONE',  ( -40.00000000000000000, 19.00000000000000000, 25.99999999999999645 ) ) ;
#8798=PLANE ( 'NONE',  #1751 ) ;
#8823=DIRECTION ( 'NONE',  ( -0.000000000000000000, -1.000000000000000000, -0.000000000000000000 ) ) ;
#8849=LINE ( 'NONE', #2315, #7801 ) ;
#8854=MECHANICAL_DESIGN_GEOMETRIC_PRESENTATION_REPRESENTATION('',(#4201),#16263);
#8858=DIRECTION ( 'NONE',  ( -0.000000000000000000, -1.000000000000000000, -0.000000000000000000 ) ) ;
#8859=ORIENTED_EDGE ( 'NONE', *, *, #1765, .F. ) ;
#8865=ORIENTED_EDGE ( 'NONE', *, *, #9670, .F. ) ;
#8891=LINE ( 'NONE', #3565, #1569 ) ;
#8897=EDGE_CURVE ( 'NONE', #1411, #1755, #9331, .T. ) ;
#8902=FACE_OUTER_BOUND ( 'NONE', #4331, .T. ) ;
#8909=CYLINDRICAL_SURFACE ( 'NONE', #16550, 3.300000000000000711 ) ;
#8937=FACE_OUTER_BOUND ( 'NONE', #657, .T. ) ;
#8947=DIRECTION ( 'NONE',  ( 0.000000000000000000, 0.000000000000000000, 1.000000000000000000 ) ) ;
#8950=CARTESIAN_POINT ( 'NONE',  ( 31.81980515339464333, 0.000000000000000000, -31.81980515339463622 ) ) ;
#8960=ORIENTED_EDGE ( 'NONE', *, *, #7781, .F. ) ;
#8968=LINE ( 'NONE', #2507, #16561 ) ;
#8973=VERTEX_POINT ( 'NONE', #13638 ) ;
#8980=FACE_OUTER_BOUND ( 'NONE', #7158, .T. ) ;
#8983=AXIS2_PLACEMENT_3D ( 'NONE', #10386, #10306, #3780 ) ;
#9000=PLANE ( 'NONE',  #13986 ) ;
#9003=DIRECTION ( 'NONE',  ( 0.000000000000000000, 0.000000000000000000, 1.000000000000000000 ) ) ;
#9021=DIRECTION ( 'NONE',  ( 0.000000000000000000, 0.000000000000000000, 1.000000000000000000 ) ) ;
#9033=EDGE_LOOP ( 'NONE', ( #395, #1090 ) ) ;
#9042=ORIENTED_EDGE ( 'NONE', *, *, #2966, .T. ) ;
#9043=CARTESIAN_POINT ( 'NONE',  ( 40.00000000000000711, 8.000000000000000000, -34.99999999999997868 ) ) ;
#9048=CARTESIAN_POINT ( 'NONE',  ( -31.00000000000000000, 19.00000000000000000, -31.00000000000000000 ) ) ;
#9058=EDGE_LOOP ( 'NONE', ( #6392, #160, #4648, #10997 ) ) ;
#9059=VERTEX_POINT ( 'NONE', #13710 ) ;
#9090=CARTESIAN_POINT ( 'NONE',  ( 26.00000000000000000, 19.00000000000000000, -40.00000000000000711 ) ) ;
#9094=CARTESIAN_POINT ( 'NONE',  ( 35.00000000000000711, 19.00000000000000000, 20.99999999999999289 ) ) ;
#9096=DIRECTION ( 'NONE',  ( 0.000000000000000000, 0.000000000000000000, -1.000000000000000000 ) ) ;
#9100=EDGE_CURVE ( 'NONE', #4422, #4924, #12756, .T. ) ;
#9101=CYLINDRICAL_SURFACE ( 'NONE', #2038, 3.299999999999997158 ) ;
#9119=EDGE_LOOP ( 'NONE', ( #15072, #3380, #15486, #8192 ) ) ;
#9120=AXIS2_PLACEMENT_3D ( 'NONE', #10144, #3787, #3616 ) ;
#9125=ORIENTED_EDGE ( 'NONE', *, *, #4876, .F. ) ;
#9132=DIRECTION ( 'NONE',  ( -0.000000000000000000, -1.000000000000000000, -0.000000000000000000 ) ) ;
#9144=EDGE_CURVE ( 'NONE', #11543, #10620, #10351, .T. ) ;
#9147=VECTOR ( 'NONE', #9898, 1000.000000000000000 ) ;
#9149=ORIENTED_EDGE ( 'NONE', *, *, #695, .F. ) ;
#9169=ORIENTED_EDGE ( 'NONE', *, *, #13083, .F. ) ;
#9179=FACE_OUTER_BOUND ( 'NONE', #1686, .T. ) ;
#9180=APPLICATION_CONTEXT ( 'automotive_design' ) ;
#9187=DIRECTION ( 'NONE',  ( 0.000000000000000000, 0.000000000000000000, -1.000000000000000000 ) ) ;
#9206=LINE ( 'NONE', #11511, #12181 ) ;
#9243=DIRECTION ( 'NONE',  ( 0.000000000000000000, -1.000000000000000000, 0.000000000000000000 ) ) ;
#9248=FACE_OUTER_BOUND ( 'NONE', #2389, .T. ) ;
#9249=CARTESIAN_POINT ( 'NONE',  ( -35.00000000000000000, 19.00000000000000000, 20.99999999999999289 ) ) ;
#9278=CARTESIAN_POINT ( 'NONE',  ( 35.00000000000000711, 8.000000000000000000, -21.00000000000000355 ) ) ;
#9281=ORIENTED_EDGE ( 'NONE', *, *, #10864, .T. ) ;
#9283=CARTESIAN_POINT ( 'NONE',  ( 4.286263797015737285E-15, 0.000000000000000000, -35.00000000000000711 ) ) ;
#9284=PLANE ( 'NONE',  #5123 ) ;
#9287=VECTOR ( 'NONE', #5795, 1000.000000000000000 ) ;
#9331=CIRCLE ( 'NONE', #7118, 3.300000000000004263 ) ;
#9343=DIRECTION ( 'NONE',  ( 0.000000000000000000, 0.000000000000000000, 1.000000000000000000 ) ) ;
#9344=DIRECTION ( 'NONE',  ( 0.000000000000000000, 1.000000000000000000, 0.000000000000000000 ) ) ;
#9364=ORIENTED_EDGE ( 'NONE', *, *, #13100, .F. ) ;
#9367=FACE_OUTER_BOUND ( 'NONE', #9825, .T. ) ;
#9369=ADVANCED_FACE ( 'NONE', ( #11594, #2661 ), #1213, .T. ) ;
#9373=ORIENTED_EDGE ( 'NONE', *, *, #8897, .T. ) ;
#9378=ORIENTED_EDGE ( 'NONE', *, *, #4583, .F. ) ;
#9384=EDGE_CURVE ( 'NONE', #16924, #16617, #14186, .T. ) ;
#9404=CARTESIAN_POINT ( 'NONE',  ( 0.000000000000000000, -3.000000000000000000, 0.000000000000000000 ) ) ;
#9407=CARTESIAN_POINT ( 'NONE',  ( 0.000000000000000000, 19.00100000000000122, -18.50000000000000000 ) ) ;
#9412=ADVANCED_FACE ( 'NONE', ( #16828 ), #1122, .F. ) ;
#9414=DIRECTION ( 'NONE',  ( -0.000000000000000000, -0.000000000000000000, 1.000000000000000000 ) ) ;
#9437=CARTESIAN_POINT ( 'NONE',  ( 31.81980515339464333, 11.00000000000000000, -28.51980515339463906 ) ) ;
#9450=VECTOR ( 'NONE', #13165, 1000.000000000000000 ) ;
#9456=FACE_OUTER_BOUND ( 'NONE', #3639, .T. ) ;
#9467=ORIENTED_EDGE ( 'NONE', *, *, #10367, .T. ) ;
#9468=CARTESIAN_POINT ( 'NONE',  ( 21.00000000000000000, 19.00000000000000000, 35.00000000000001421 ) ) ;
#9469=AXIS2_PLACEMENT_3D ( 'NONE', #6586, #5396, #14595 ) ;
#9470=EDGE_LOOP ( 'NONE', ( #2688, #4406, #6885, #1915 ) ) ;
#9478=EDGE_LOOP ( 'NONE', ( #1100, #14645 ) ) ;
#9508=LINE ( 'NONE', #15933, #6917 ) ;
#9509=EDGE_CURVE ( 'NONE', #13438, #9059, #12005, .T. ) ;
#9522=DIRECTION ( 'NONE',  ( 0.000000000000000000, 0.000000000000000000, 1.000000000000000000 ) ) ;
#9527=ORIENTED_EDGE ( 'NONE', *, *, #13100, .T. ) ;
#9534=CYLINDRICAL_SURFACE ( 'NONE', #11299, 35.00000000000000711 ) ;
#9550=ORIENTED_EDGE ( 'NONE', *, *, #4992, .T. ) ;
#9552=ORIENTED_EDGE ( 'NONE', *, *, #11904, .T. ) ;
#9569=EDGE_CURVE ( 'NONE', #2054, #1839, #4100, .T. ) ;
#9570=ORIENTED_EDGE ( 'NONE', *, *, #4464, .F. ) ;
#9572=CARTESIAN_POINT ( 'NONE',  ( 40.00000000000000711, 0.000000000000000000, -34.99999999999997868 ) ) ;
#9578=ORIENTED_EDGE ( 'NONE', *, *, #6533, .F. ) ;
#9585=DIRECTION ( 'NONE',  ( 0.000000000000000000, 1.000000000000000000, -0.000000000000000000 ) ) ;
#9588=DIRECTION ( 'NONE',  ( -0.000000000000000000, -0.000000000000000000, 1.000000000000000000 ) ) ;
#9594=LINE ( 'NONE', #12336, #5071 ) ;
#9600=EDGE_CURVE ( 'NONE', #4853, #15712, #4896, .T. ) ;
#9621=DIRECTION ( 'NONE',  ( 0.000000000000000000, 0.000000000000000000, -1.000000000000000000 ) ) ;
#9635=VECTOR ( 'NONE', #11824, 1000.000000000000000 ) ;
#9656=VERTEX_POINT ( 'NONE', #4282 ) ;
#9659=ORIENTED_EDGE ( 'NONE', *, *, #264, .T. ) ;
#9661=VERTEX_POINT ( 'NONE', #2981 ) ;
#9664=AXIS2_PLACEMENT_3D ( 'NONE', #15578, #6367, #987 ) ;
#9670=EDGE_CURVE ( 'NONE', #10121, #3447, #7411, .T. ) ;
#9672=CARTESIAN_POINT ( 'NONE',  ( -34.99999999999999289, 0.000000000000000000, -35.00000000000000711 ) ) ;
#9675=CYLINDRICAL_SURFACE ( 'NONE', #8328, 18.50000000000000000 ) ;
#9680=VECTOR ( 'NONE', #13623, 1000.000000000000000 ) ;
#9682=CARTESIAN_POINT ( 'NONE',  ( 40.00000000000000711, 19.00000000000000000, 25.99999999999999645 ) ) ;
#9690=DIRECTION ( 'NONE',  ( -0.000000000000000000, -1.000000000000000000, -0.000000000000000000 ) ) ;
#9709=LINE ( 'NONE', #1550, #16710 ) ;
#9715=AXIS2_PLACEMENT_3D ( 'NONE', #10951, #4426, #3387 ) ;
#9743=ORIENTED_EDGE ( 'NONE', *, *, #600, .T. ) ;
#9746=APPLICATION_CONTEXT ( 'automotive_design' ) ;
#9748=ORIENTED_EDGE ( 'NONE', *, *, #10244, .T. ) ;
#9774=ORIENTED_EDGE ( 'NONE', *, *, #14747, .F. ) ;
#9788=DIRECTION ( 'NONE',  ( 0.000000000000000000, 0.000000000000000000, 1.000000000000000000 ) ) ;
#9789=LINE ( 'NONE', #4543, #12009 ) ;
#9825=EDGE_LOOP ( 'NONE', ( #9743, #9378, #11741, #6171 ) ) ;
#9836=DIRECTION ( 'NONE',  ( -1.000000000000000000, 0.000000000000000000, -0.000000000000000000 ) ) ;
#9837=CARTESIAN_POINT ( 'NONE',  ( -34.99999999999999289, 11.00000000000000000, 40.00000000000000711 ) ) ;
#9856=EDGE_LOOP ( 'NONE', ( #5703, #12562 ) ) ;
#9881=ORIENTED_EDGE ( 'NONE', *, *, #806, .T. ) ;
#9885=ORIENTED_EDGE ( 'NONE', *, *, #6250, .F. ) ;
#9888=VECTOR ( 'NONE', #6926, 1000.000000000000000 ) ;
#9898=DIRECTION ( 'NONE',  ( -0.000000000000000000, -1.000000000000000000, -0.000000000000000000 ) ) ;
#9907=ORIENTED_EDGE ( 'NONE', *, *, #15589, .T. ) ;
#9921=CARTESIAN_POINT ( 'NONE',  ( 26.00000000000000000, 19.00000000000000000, -40.00000000000000711 ) ) ;
#9923=AXIS2_PLACEMENT_3D ( 'NONE', #14848, #4198, #10716 ) ;
#9937=EDGE_CURVE ( 'NONE', #11353, #9952, #16949, .T. ) ;
#9941=AXIS2_PLACEMENT_3D ( 'NONE', #15268, #4615, #11148 ) ;
#9942=AXIS2_PLACEMENT_3D ( 'NONE', #11944, #11762, #2482 ) ;
#9948=DIRECTION ( 'NONE',  ( -1.000000000000000000, -0.000000000000000000, -0.000000000000000000 ) ) ;
#9952=VERTEX_POINT ( 'NONE', #10519 ) ;
#9954=DIRECTION ( 'NONE',  ( 0.000000000000000000, 0.000000000000000000, 1.000000000000000000 ) ) ;
#9975=EDGE_CURVE ( 'NONE', #4897, #16617, #14481, .T. ) ;
#9982=ORIENTED_EDGE ( 'NONE', *, *, #2015, .T. ) ;
#10001=LINE ( 'NONE', #15061, #10451 ) ;
#10003=CARTESIAN_POINT ( 'NONE',  ( -31.81980515339462912, 0.000000000000000000, 35.11980515339465825 ) ) ;
#10006=CARTESIAN_POINT ( 'NONE',  ( 26.00000000000000355, 19.00000000000000000, -31.00000000000004263 ) ) ;
#10012=DIRECTION ( 'NONE',  ( 0.000000000000000000, 0.000000000000000000, -1.000000000000000000 ) ) ;
#10015=ORIENTED_EDGE ( 'NONE', *, *, #14747, .T. ) ;
#10044=ORIENTED_EDGE ( 'NONE', *, *, #13682, .F. ) ;
#10050=CARTESIAN_POINT ( 'NONE',  ( 31.00000000000000000, 19.00000000000000000, -31.00000000000000355 ) ) ;
#10056=DIRECTION ( 'NONE',  ( -0.000000000000000000, -0.000000000000000000, 1.000000000000000000 ) ) ;
#10068=AXIS2_PLACEMENT_3D ( 'NONE', #12515, #8406, #11224 ) ;
#10070=DIRECTION ( 'NONE',  ( -0.000000000000000000, -1.000000000000000000, -0.000000000000000000 ) ) ;
#10072=CARTESIAN_POINT ( 'NONE',  ( -35.00000000000000000, 19.00000000000000000, -21.00000000000000000 ) ) ;
#10099=DIRECTION ( 'NONE',  ( 0.000000000000000000, -0.000000000000000000, 1.000000000000000000 ) ) ;
#10109=ORIENTED_EDGE ( 'NONE', *, *, #9975, .F. ) ;
#10114=PLANE ( 'NONE',  #13253 ) ;
#10121=VERTEX_POINT ( 'NONE', #3226 ) ;
#10122=FACE_OUTER_BOUND ( 'NONE', #5012, .T. ) ;
#10132=ORIENTED_EDGE ( 'NONE', *, *, #2792, .F. ) ;
#10134=DIRECTION ( 'NONE',  ( -0.000000000000000000, -1.000000000000000000, -0.000000000000000000 ) ) ;
#10144=CARTESIAN_POINT ( 'NONE',  ( 31.00000000000000000, 8.000000000000000000, -31.00000000000000355 ) ) ;
#10148=EDGE_CURVE ( 'NONE', #2164, #12818, #2878, .T. ) ;
#10152=LINE ( 'NONE', #15308, #14425 ) ;
#10169=CARTESIAN_POINT ( 'NONE',  ( -26.00000000000000000, 11.00000000000000000, 40.00000000000000711 ) ) ;
#10171=DIRECTION ( 'NONE',  ( 0.000000000000000000, 0.000000000000000000, -1.000000000000000000 ) ) ;
#10173=DIRECTION ( 'NONE',  ( 0.000000000000000000, 1.000000000000000000, 0.000000000000000000 ) ) ;
#10182=EDGE_CURVE ( 'NONE', #11977, #15142, #3302, .T. ) ;
#10223=EDGE_CURVE ( 'NONE', #4822, #10494, #10001, .T. ) ;
#10226=COLOUR_RGB ( '', 0.72549020, 0.75294118, 0.79215686) ;
#10232=CARTESIAN_POINT ( 'NONE',  ( -39.99999999999999289, 8.000000000000000000, 34.99999999999997868 ) ) ;
#10241=VECTOR ( 'NONE', #1665, 1000.000000000000000 ) ;
#10244=EDGE_CURVE ( 'NONE', #8973, #9661, #13697, .T. ) ;
#10264=PLANE ( 'NONE',  #13652 ) ;
#10275=VECTOR ( 'NONE', #16163, 1000.000000000000000 ) ;
#10284=DIRECTION ( 'NONE',  ( -0.000000000000000000, -1.000000000000000000, -0.000000000000000000 ) ) ;
#10304=VERTEX_POINT ( 'NONE', #4835 ) ;
#10306=DIRECTION ( 'NONE',  ( 0.000000000000000000, 1.000000000000000000, 0.000000000000000000 ) ) ;
#10307=PLANE ( 'NONE',  #13222 ) ;
#10308=ORIENTED_EDGE ( 'NONE', *, *, #10223, .F. ) ;
#10316=VECTOR ( 'NONE', #4030, 1000.000000000000000 ) ;
#10331=AXIS2_PLACEMENT_3D ( 'NONE', #5901, #7262, #5731 ) ;
#10337=DIRECTION ( 'NONE',  ( -0.000000000000000000, -1.000000000000000000, -0.000000000000000000 ) ) ;
#10342=VECTOR ( 'NONE', #7331, 1000.000000000000000 ) ;
#10343=EDGE_CURVE ( 'NONE', #2412, #11631, #3893, .T. ) ;
#10351=LINE ( 'NONE', #13011, #8519 ) ;
#10353=FACE_BOUND ( 'NONE', #11189, .T. ) ;
#10367=EDGE_CURVE ( 'NONE', #742, #12007, #3614, .T. ) ;
#10372=DIRECTION ( 'NONE',  ( 0.000000000000000000, 0.000000000000000000, 1.000000000000000000 ) ) ;
#10385=VERTEX_POINT ( 'NONE', #1231 ) ;
#10386=CARTESIAN_POINT ( 'NONE',  ( 31.81980515339464333, 11.00000000000000000, -31.81980515339463622 ) ) ;
#10396=DIRECTION ( 'NONE',  ( -1.000000000000000000, 0.000000000000000000, -0.000000000000000000 ) ) ;
#10398=CARTESIAN_POINT ( 'NONE',  ( 31.00000000000000000, 19.00000000000000000, 30.99999999999999289 ) ) ;
#10401=DIRECTION ( 'NONE',  ( 1.000000000000000000, -0.000000000000000000, 0.000000000000000000 ) ) ;
#10402=ORIENTED_EDGE ( 'NONE', *, *, #13061, .T. ) ;
#10404=VERTEX_POINT ( 'NONE', #5083 ) ;
#10446=ORIENTED_EDGE ( 'NONE', *, *, #15997, .T. ) ;
#10451=VECTOR ( 'NONE', #3386, 1000.000000000000000 ) ;
#10460=VERTEX_POINT ( 'NONE', #8358 ) ;
#10472=ADVANCED_FACE ( 'NONE', ( #5767, #1743, #3122, #10752, #16162, #15898 ), #14717, .T. ) ;
#10479=VERTEX_POINT ( 'NONE', #1573 ) ;
#10493=VECTOR ( 'NONE', #11484, 1000.000000000000000 ) ;
#10494=VERTEX_POINT ( 'NONE', #6967 ) ;
#10505=AXIS2_PLACEMENT_3D ( 'NONE', #15083, #15173, #7419 ) ;
#10516=VECTOR ( 'NONE', #14485, 1000.000000000000000 ) ;
#10519=CARTESIAN_POINT ( 'NONE',  ( -20.99999999999999645, 8.000000000000000000, -35.00000000000000711 ) ) ;
#10521=VERTEX_POINT ( 'NONE', #5506 ) ;
#10530=AXIS2_PLACEMENT_3D ( 'NONE', #13670, #1820, #704 ) ;
#10538=VECTOR ( 'NONE', #7156, 1000.000000000000000 ) ;
#10544=ADVANCED_FACE ( 'NONE', ( #13347 ), #4235, .T. ) ;
#10550=VECTOR ( 'NONE', #1646, 1000.000000000000000 ) ;
#10558=DIRECTION ( 'NONE',  ( -0.000000000000000000, -1.000000000000000000, -0.000000000000000000 ) ) ;
#10574=EDGE_CURVE ( 'NONE', #15142, #6773, #10931, .T. ) ;
#10577=ORIENTED_EDGE ( 'NONE', *, *, #5406, .F. ) ;
#10581=EDGE_LOOP ( 'NONE', ( #3211, #1790, #3506, #10740 ) ) ;
#10593=ORIENTED_EDGE ( 'NONE', *, *, #14025, .T. ) ;
#10599=AXIS2_PLACEMENT_3D ( 'NONE', #6998, #2798, #2971 ) ;
#10608=DIRECTION ( 'NONE',  ( -1.000000000000000000, -0.000000000000000000, -0.000000000000000000 ) ) ;
#10619=DIRECTION ( 'NONE',  ( 0.000000000000000000, 1.000000000000000000, 0.000000000000000000 ) ) ;
#10620=VERTEX_POINT ( 'NONE', #15304 ) ;
#10621=VERTEX_POINT ( 'NONE', #7460 ) ;
#10622=VECTOR ( 'NONE', #949, 1000.000000000000000 ) ;
#10639=ORIENTED_EDGE ( 'NONE', *, *, #900, .F. ) ;
#10670=CARTESIAN_POINT ( 'NONE',  ( -20.99999999999999645, 8.000000000000000000, 35.00000000000001421 ) ) ;
#10676=VECTOR ( 'NONE', #232, 1000.000000000000000 ) ;
#10703=EDGE_LOOP ( 'NONE', ( #11851, #9527, #4987, #2156 ) ) ;
#10709=VECTOR ( 'NONE', #14439, 1000.000000000000000 ) ;
#10714=CARTESIAN_POINT ( 'NONE',  ( -26.00000000000000000, 19.00000000000000000, -31.00000000000003908 ) ) ;
#10716=DIRECTION ( 'NONE',  ( 0.000000000000000000, 0.000000000000000000, -1.000000000000000000 ) ) ;
#10722=PRODUCT_DEFINITION_CONTEXT ( 'detailed design', #9180, 'design' ) ;
#10740=ORIENTED_EDGE ( 'NONE', *, *, #14239, .T. ) ;
#10752=FACE_OUTER_BOUND ( 'NONE', #4935, .T. ) ;
#10759=VECTOR ( 'NONE', #15628, 1000.000000000000000 ) ;
#10760=CARTESIAN_POINT ( 'NONE',  ( 40.00000000000000711, 0.000000000000000000, 34.99999999999997868 ) ) ;
#10770=VECTOR ( 'NONE', #7780, 1000.000000000000000 ) ;
#10784=CARTESIAN_POINT ( 'NONE',  ( -20.99999999999999645, 19.00000000000000000, -31.00000000000003908 ) ) ;
#10788=LINE ( 'NONE', #2972, #1721 ) ;
#10791=EDGE_CURVE ( 'NONE', #3447, #2369, #6422, .T. ) ;
#10798=AXIS2_PLACEMENT_3D ( 'NONE', #9672, #4744, #15062 ) ;
#10803=EDGE_LOOP ( 'NONE', ( #6698, #6469, #825, #16061 ) ) ;
#10832=CARTESIAN_POINT ( 'NONE',  ( -31.81980515339462912, 0.000000000000000000, -35.11980515339465114 ) ) ;
#10836=ORIENTED_EDGE ( 'NONE', *, *, #16531, .T. ) ;
#10837=DIRECTION ( 'NONE',  ( -1.000000000000000000, 0.000000000000000000, 0.000000000000000000 ) ) ;
#10844=ORIENTED_EDGE ( 'NONE', *, *, #264, .F. ) ;
#10845=CARTESIAN_POINT ( 'NONE',  ( 35.00000000000000711, 19.00000000000000000, 20.99999999999999289 ) ) ;
#10850=DIRECTION ( 'NONE',  ( 0.000000000000000000, -0.000000000000000000, -1.000000000000000000 ) ) ;
#10853=ORIENTED_EDGE ( 'NONE', *, *, #3116, .F. ) ;
#10854=DIRECTION ( 'NONE',  ( 0.000000000000000000, 0.000000000000000000, 1.000000000000000000 ) ) ;
#10860=VECTOR ( 'NONE', #16592, 1000.000000000000000 ) ;
#10864=EDGE_CURVE ( 'NONE', #6790, #13878, #13522, .T. ) ;
#10888=AXIS2_PLACEMENT_3D ( 'NONE', #13212, #9344, #13310 ) ;
#10892=ADVANCED_FACE ( 'NONE', ( #5402 ), #10913, .F. ) ;
#10903=CIRCLE ( 'NONE', #8149, 4.999999999999997335 ) ;
#10910=SURFACE_STYLE_USAGE ( .BOTH. , #1884 ) ;
#10913=CYLINDRICAL_SURFACE ( 'NONE', #11846, 3.299999999999997158 ) ;
#10917=DIRECTION ( 'NONE',  ( -1.000000000000000000, 0.000000000000000000, 0.000000000000000000 ) ) ;
#10924=DIRECTION ( 'NONE',  ( -0.000000000000000000, -1.000000000000000000, -0.000000000000000000 ) ) ;
#10931=LINE ( 'NONE', #10670, #605 ) ;
#10933=ORIENTED_EDGE ( 'NONE', *, *, #8109, .F. ) ;
#10948=ORIENTED_EDGE ( 'NONE', *, *, #2792, .T. ) ;
#10951=CARTESIAN_POINT ( 'NONE',  ( -31.00000000000000000, 19.00000000000000000, 30.99999999999999289 ) ) ;
#10957=FACE_OUTER_BOUND ( 'NONE', #8004, .T. ) ;
#10959=DIRECTION ( 'NONE',  ( -1.000000000000000000, -0.000000000000000000, -0.000000000000000000 ) ) ;
#10961=VERTEX_POINT ( 'NONE', #9278 ) ;
#10990=CARTESIAN_POINT ( 'NONE',  ( -26.00000000000000000, 19.00000000000000000, 40.00000000000001421 ) ) ;
#10997=ORIENTED_EDGE ( 'NONE', *, *, #3221, .T. ) ;
#11028=ORIENTED_EDGE ( 'NONE', *, *, #3845, .T. ) ;
#11035=CARTESIAN_POINT ( 'NONE',  ( -35.00000000000000000, 19.00000000000000000, -21.00000000000000000 ) ) ;
#11048=CARTESIAN_POINT ( 'NONE',  ( 31.81980515339464333, 8.000000000000000000, -35.11980515339463693 ) ) ;
#11059=VERTEX_POINT ( 'NONE', #775 ) ;
#11064=LINE ( 'NONE', #4542, #8383 ) ;
#11066=FACE_OUTER_BOUND ( 'NONE', #5977, .T. ) ;
#11079=DIRECTION ( 'NONE',  ( 0.000000000000000000, 1.000000000000000000, 0.000000000000000000 ) ) ;
#11080=ORIENTED_EDGE ( 'NONE', *, *, #600, .F. ) ;
#11082=ADVANCED_FACE ( 'NONE', ( #11238 ), #13740, .F. ) ;
#11088=ORIENTED_EDGE ( 'NONE', *, *, #1659, .F. ) ;
#11115=ORIENTED_EDGE ( 'NONE', *, *, #16093, .F. ) ;
#11120=CARTESIAN_POINT ( 'NONE',  ( 31.00000000000003553, 19.00000000000000000, 20.99999999999999289 ) ) ;
#11131=ORIENTED_EDGE ( 'NONE', *, *, #4464, .T. ) ;
#11138=CARTESIAN_POINT ( 'NONE',  ( -35.00000000000000000, 19.00000000000000000, 20.99999999999999289 ) ) ;
#11142=CIRCLE ( 'NONE', #10888, 4.999999999999997335 ) ;
#11148=DIRECTION ( 'NONE',  ( 0.000000000000000000, 0.000000000000000000, 1.000000000000000000 ) ) ;
#11149=DIRECTION ( 'NONE',  ( -0.000000000000000000, -1.000000000000000000, -0.000000000000000000 ) ) ;
#11153=CARTESIAN_POINT ( 'NONE',  ( -31.81980515339462912, 0.000000000000000000, -31.81980515339465043 ) ) ;
#11189=EDGE_LOOP ( 'NONE', ( #14593, #7390 ) ) ;
#11199=CARTESIAN_POINT ( 'NONE',  ( 31.81980515339464333, 11.00000000000000000, 31.81980515339463622 ) ) ;
#11205=LINE ( 'NONE', #12579, #7093 ) ;
#11208=CARTESIAN_POINT ( 'NONE',  ( 21.00000000000000000, 8.000000000000000000, 31.00000000000006395 ) ) ;
#11211=SHAPE_REPRESENTATION ( 'Servo-Head', ( #1488 ), #15199 ) ;
#11224=DIRECTION ( 'NONE',  ( 0.000000000000000000, 0.000000000000000000, 1.000000000000000000 ) ) ;
#11228=DIRECTION ( 'NONE',  ( 0.000000000000000000, 0.000000000000000000, 1.000000000000000000 ) ) ;
#11238=FACE_OUTER_BOUND ( 'NONE', #7398, .T. ) ;
#11240=ORIENTED_EDGE ( 'NONE', *, *, #9937, .T. ) ;
#11243=CARTESIAN_POINT ( 'NONE',  ( -20.99999999999999645, 19.00000000000000000, -35.00000000000000711 ) ) ;
#11247=EDGE_LOOP ( 'NONE', ( #4643, #9570, #6551, #3370 ) ) ;
#11249=CARTESIAN_POINT ( 'NONE',  ( 0.000000000000000000, -3.000000000000000000, 0.000000000000000000 ) ) ;
#11262=ORIENTED_EDGE ( 'NONE', *, *, #6250, .T. ) ;
#11279=ADVANCED_FACE ( 'NONE', ( #10122 ), #7692, .T. ) ;
#11292=CARTESIAN_POINT ( 'NONE',  ( 31.81980515339464333, 0.000000000000000000, 31.81980515339463622 ) ) ;
#11299=AXIS2_PLACEMENT_3D ( 'NONE', #2822, #2998, #14771 ) ;
#11314=DIRECTION ( 'NONE',  ( 0.000000000000000000, 0.000000000000000000, -1.000000000000000000 ) ) ;
#11317=ORIENTED_EDGE ( 'NONE', *, *, #4952, .T. ) ;
#11318=LINE ( 'NONE', #12696, #3648 ) ;
#11331=CYLINDRICAL_SURFACE ( 'NONE', #5693, 18.50000000000000000 ) ;
#11339=AXIS2_PLACEMENT_3D ( 'NONE', #11120, #16357, #9836 ) ;
#11340=ADVANCED_FACE ( 'NONE', ( #9179 ), #5384, .T. ) ;
#11344=CARTESIAN_POINT ( 'NONE',  ( 21.00000000000000000, 19.00000000000000000, 31.00000000000006395 ) ) ;
#11353=VERTEX_POINT ( 'NONE', #13127 ) ;
#11355=AXIS2_PLACEMENT_3D ( 'NONE', #8128, #10619, #13378 ) ;
#11363=FACE_OUTER_BOUND ( 'NONE', #8371, .T. ) ;
#11368=CIRCLE ( 'NONE', #3978, 4.999999999999997335 ) ;
#11372=DIRECTION ( 'NONE',  ( 0.000000000000000000, 0.000000000000000000, -1.000000000000000000 ) ) ;
#11381=DIRECTION ( 'NONE',  ( 0.000000000000000000, 0.000000000000000000, 1.000000000000000000 ) ) ;
#11391=UNCERTAINTY_MEASURE_WITH_UNIT (LENGTH_MEASURE( 1.000000000000000082E-05 ), #6940, 'distance_accuracy_value', 'NONE');
#11398=LINE ( 'NONE', #16463, #5824 ) ;
#11405=EDGE_CURVE ( 'NONE', #15841, #11860, #12091, .T. ) ;
#11412=ORIENTED_EDGE ( 'NONE', *, *, #11405, .T. ) ;
#11415=ORIENTED_EDGE ( 'NONE', *, *, #900, .T. ) ;
#11446=ORIENTED_EDGE ( 'NONE', *, *, #1021, .F. ) ;
#11450=CARTESIAN_POINT ( 'NONE',  ( 31.00000000000000000, 19.00000000000000000, -31.00000000000000355 ) ) ;
#11456=CARTESIAN_POINT ( 'NONE',  ( -31.81980515339462912, 11.00000000000000000, 31.81980515339465043 ) ) ;
#11463=VECTOR ( 'NONE', #5625, 1000.000000000000000 ) ;
#11467=ORIENTED_EDGE ( 'NONE', *, *, #7924, .F. ) ;
#11480=CARTESIAN_POINT ( 'NONE',  ( 31.00000000000003908, 19.00000000000000000, -26.00000000000000355 ) ) ;
#11484=DIRECTION ( 'NONE',  ( -0.000000000000000000, -0.000000000000000000, 1.000000000000000000 ) ) ;
#11495=FACE_OUTER_BOUND ( 'NONE', #7221, .T. ) ;
#11498=EDGE_CURVE ( 'NONE', #11860, #4422, #981, .T. ) ;
#11511=CARTESIAN_POINT ( 'NONE',  ( 40.00000000000000711, 11.00000000000000000, -26.00000000000000355 ) ) ;
#11524=ORIENTED_EDGE ( 'NONE', *, *, #6418, .F. ) ;
#11526=VERTEX_POINT ( 'NONE', #3644 ) ;
#11527=CIRCLE ( 'NONE', #265, 18.50000000000000000 ) ;
#11542=DIRECTION ( 'NONE',  ( 0.000000000000000000, 0.000000000000000000, 1.000000000000000000 ) ) ;
#11543=VERTEX_POINT ( 'NONE', #5960 ) ;
#11545=DIRECTION ( 'NONE',  ( -0.000000000000000000, -1.000000000000000000, -0.000000000000000000 ) ) ;
#11550=ORIENTED_EDGE ( 'NONE', *, *, #4156, .T. ) ;
#11552=CIRCLE ( 'NONE', #11853, 3.300000000000004263 ) ;
#11580=DIRECTION ( 'NONE',  ( 0.000000000000000000, 0.000000000000000000, 1.000000000000000000 ) ) ;
#11587=VECTOR ( 'NONE', #11372, 1000.000000000000000 ) ;
#11591=CIRCLE ( 'NONE', #9664, 18.50000000000000000 ) ;
#11594=FACE_OUTER_BOUND ( 'NONE', #16919, .T. ) ;
#11603=VECTOR ( 'NONE', #15906, 1000.000000000000000 ) ;
#11616=AXIS2_PLACEMENT_3D ( 'NONE', #12310, #8782, #8616 ) ;
#11631=VERTEX_POINT ( 'NONE', #2506 ) ;
#11636=EDGE_LOOP ( 'NONE', ( #11317, #471, #7295, #4391, #14648, #11412, #15859, #6604, #5324, #7202, #211, #5505, #7862, #1136, #7200, #14113 ) ) ;
#11646=PRODUCT_DEFINITION_FORMATION_WITH_SPECIFIED_SOURCE ( 'ANY', '', #4910, .NOT_KNOWN. ) ;
#11654=ORIENTED_EDGE ( 'NONE', *, *, #566, .F. ) ;
#11660=AXIS2_PLACEMENT_3D ( 'NONE', #12085, #324, #14756 ) ;
#11678=( LENGTH_UNIT ( ) NAMED_UNIT ( * ) SI_UNIT ( .MILLI., .METRE. ) );
#11705=ORIENTED_EDGE ( 'NONE', *, *, #1549, .F. ) ;
#11727=EDGE_LOOP ( 'NONE', ( #5387, #2500, #9659, #4716, #5813, #5441, #15025, #16823, #534, #9467, #14300, #5120, #10402, #9281, #835, #11240 ) ) ;
#11733=FACE_OUTER_BOUND ( 'NONE', #10703, .T. ) ;
#11741=ORIENTED_EDGE ( 'NONE', *, *, #16844, .F. ) ;
#11748=EDGE_CURVE ( 'NONE', #13878, #11353, #13519, .T. ) ;
#11750=ORIENTED_EDGE ( 'NONE', *, *, #13369, .F. ) ;
#11762=DIRECTION ( 'NONE',  ( -0.000000000000000000, -1.000000000000000000, -0.000000000000000000 ) ) ;
#11774=EDGE_LOOP ( 'NONE', ( #638, #4502, #15910, #1238 ) ) ;
#11778=ADVANCED_FACE ( 'NONE', ( #14974, #8099 ), #8444, .F. ) ;
#11809=ORIENTED_EDGE ( 'NONE', *, *, #4992, .F. ) ;
#11814=FACE_OUTER_BOUND ( 'NONE', #6588, .T. ) ;
#11824=DIRECTION ( 'NONE',  ( -0.000000000000000000, 1.000000000000000000, -0.000000000000000000 ) ) ;
#11837=DIRECTION ( 'NONE',  ( -0.000000000000000000, -1.000000000000000000, -0.000000000000000000 ) ) ;
#11846=AXIS2_PLACEMENT_3D ( 'NONE', #6945, #267, #95 ) ;
#11849=PLANE ( 'NONE',  #12477 ) ;
#11851=ORIENTED_EDGE ( 'NONE', *, *, #5790, .T. ) ;
#11853=AXIS2_PLACEMENT_3D ( 'NONE', #13894, #15182, #11228 ) ;
#11856=DIRECTION ( 'NONE',  ( 0.000000000000000000, 1.000000000000000000, -0.000000000000000000 ) ) ;
#11860=VERTEX_POINT ( 'NONE', #209 ) ;
#11872=DIRECTION ( 'NONE',  ( 0.000000000000000000, 0.000000000000000000, 1.000000000000000000 ) ) ;
#11881=VECTOR ( 'NONE', #10056, 1000.000000000000000 ) ;
#11882=CARTESIAN_POINT ( 'NONE',  ( -31.00000000000003197, 19.00000000000000000, -26.00000000000000355 ) ) ;
#11900=DIRECTION ( 'NONE',  ( -0.000000000000000000, -1.000000000000000000, -0.000000000000000000 ) ) ;
#11904=EDGE_CURVE ( 'NONE', #12818, #6752, #5690, .T. ) ;
#11905=CARTESIAN_POINT ( 'NONE',  ( -34.99999999999996447, 8.000000000000000000, 40.00000000000000711 ) ) ;
#11913=ORIENTED_EDGE ( 'NONE', *, *, #7944, .F. ) ;
#11916=CARTESIAN_POINT ( 'NONE',  ( -39.99999999999999289, 11.00000000000000000, 34.99999999999997868 ) ) ;
#11944=CARTESIAN_POINT ( 'NONE',  ( 31.81980515339464333, 8.000000000000000000, 31.81980515339463622 ) ) ;
#11957=ORIENTED_EDGE ( 'NONE', *, *, #1566, .T. ) ;
#11976=CARTESIAN_POINT ( 'NONE',  ( 26.00000000000000000, 19.00000000000000000, 40.00000000000001421 ) ) ;
#11977=VERTEX_POINT ( 'NONE', #797 ) ;
#11985=ORIENTED_EDGE ( 'NONE', *, *, #10244, .F. ) ;
#11986=DIRECTION ( 'NONE',  ( -0.000000000000000000, -1.000000000000000000, -0.000000000000000000 ) ) ;
#11994=LINE ( 'NONE', #12165, #10676 ) ;
#11998=DIRECTION ( 'NONE',  ( 0.000000000000000000, 0.000000000000000000, 1.000000000000000000 ) ) ;
#12005=LINE ( 'NONE', #2636, #14829 ) ;
#12006=PLANE ( 'NONE',  #6104 ) ;
#12007=VERTEX_POINT ( 'NONE', #3287 ) ;
#12009=VECTOR ( 'NONE', #15019, 1000.000000000000000 ) ;
#12021=CARTESIAN_POINT ( 'NONE',  ( -31.81980515339462912, 11.00000000000000000, 28.51980515339464617 ) ) ;
#12054=DIRECTION ( 'NONE',  ( 0.000000000000000000, 0.000000000000000000, -1.000000000000000000 ) ) ;
#12085=CARTESIAN_POINT ( 'NONE',  ( -34.99999999999999289, 0.000000000000000000, 35.00000000000000711 ) ) ;
#12091=LINE ( 'NONE', #331, #12964 ) ;
#12108=CARTESIAN_POINT ( 'NONE',  ( 40.00000000000000711, 19.00000000000000000, 25.99999999999999645 ) ) ;
#12111=DIRECTION ( 'NONE',  ( 0.000000000000000000, 0.000000000000000000, 1.000000000000000000 ) ) ;
#12126=EDGE_CURVE ( 'NONE', #7102, #13859, #9206, .T. ) ;
#12131=EDGE_LOOP ( 'NONE', ( #1499, #4379, #5172, #8665, #5845, #3138, #1306, #15690 ) ) ;
#12141=EDGE_CURVE ( 'NONE', #13213, #10404, #5325, .T. ) ;
#12143=EDGE_LOOP ( 'NONE', ( #6895, #13050, #8481, #2422 ) ) ;
#12144=FACE_OUTER_BOUND ( 'NONE', #1221, .T. ) ;
#12150=EDGE_CURVE ( 'NONE', #16617, #3282, #4756, .T. ) ;
#12165=CARTESIAN_POINT ( 'NONE',  ( 31.00000000000006750, 8.000000000000000000, -21.00000000000000355 ) ) ;
#12181=VECTOR ( 'NONE', #16748, 1000.000000000000000 ) ;
#12194=ORIENTED_EDGE ( 'NONE', *, *, #10343, .T. ) ;
#12200=SURFACE_STYLE_FILL_AREA ( #16060 ) ;
#12213=CARTESIAN_POINT ( 'NONE',  ( 26.00000000000000355, 11.00000000000000000, -40.00000000000000711 ) ) ;
#12218=VERTEX_POINT ( 'NONE', #14604 ) ;
#12220=EDGE_LOOP ( 'NONE', ( #1733, #16259 ) ) ;
#12229=VERTEX_POINT ( 'NONE', #526 ) ;
#12243=DIRECTION ( 'NONE',  ( 0.000000000000000000, 0.000000000000000000, -1.000000000000000000 ) ) ;
#12254=CIRCLE ( 'NONE', #12513, 3.300000000000004263 ) ;
#12257=CARTESIAN_POINT ( 'NONE',  ( 40.00000000000000711, 19.00000000000000000, -26.00000000000000355 ) ) ;
#12258=LINE ( 'NONE', #492, #14893 ) ;
#12285=EDGE_LOOP ( 'NONE', ( #16942, #970, #358, #8237 ) ) ;
#12303=DIRECTION ( 'NONE',  ( 0.000000000000000000, -0.000000000000000000, -1.000000000000000000 ) ) ;
#12310=CARTESIAN_POINT ( 'NONE',  ( -31.00000000000000000, 19.00000000000000000, -31.00000000000000000 ) ) ;
#12312=LINE ( 'NONE', #4501, #11881 ) ;
#12326=CARTESIAN_POINT ( 'NONE',  ( 31.00000000000000000, 11.00000000000000000, -26.00000000000000355 ) ) ;
#12328=CYLINDRICAL_SURFACE ( 'NONE', #13126, 3.299999999999997158 ) ;
#12334=ORIENTED_EDGE ( 'NONE', *, *, #4583, .T. ) ;
#12336=CARTESIAN_POINT ( 'NONE',  ( 40.00000000000000711, 11.00000000000000000, 25.99999999999999645 ) ) ;
#12352=VECTOR ( 'NONE', #10134, 1000.000000000000000 ) ;
#12390=CARTESIAN_POINT ( 'NONE',  ( 26.00000000000000000, 19.00000000000000000, 31.00000000000003197 ) ) ;
#12398=VECTOR ( 'NONE', #13321, 1000.000000000000000 ) ;
#12430=VERTEX_POINT ( 'NONE', #3520 ) ;
#12436=VECTOR ( 'NONE', #7965, 1000.000000000000000 ) ;
#12444=DIRECTION ( 'NONE',  ( -1.000000000000000000, 0.000000000000000000, 0.000000000000000000 ) ) ;
#12466=AXIS2_PLACEMENT_3D ( 'NONE', #872, #12632, #10396 ) ;
#12473=LINE ( 'NONE', #625, #10275 ) ;
#12477=AXIS2_PLACEMENT_3D ( 'NONE', #4214, #12111, #14437 ) ;
#12482=ORIENTED_EDGE ( 'NONE', *, *, #1324, .T. ) ;
#12513=AXIS2_PLACEMENT_3D ( 'NONE', #5993, #11079, #8501 ) ;
#12515=CARTESIAN_POINT ( 'NONE',  ( 31.81980515339464333, 0.000000000000000000, -31.81980515339463622 ) ) ;
#12518=DIRECTION ( 'NONE',  ( -0.000000000000000000, -0.000000000000000000, 1.000000000000000000 ) ) ;
#12541=CARTESIAN_POINT ( 'NONE',  ( 26.00000000000000355, 19.00000000000000000, -31.00000000000003908 ) ) ;
#12556=ORIENTED_EDGE ( 'NONE', *, *, #13490, .T. ) ;
#12562=ORIENTED_EDGE ( 'NONE', *, *, #10343, .F. ) ;
#12570=DIRECTION ( 'NONE',  ( -1.000000000000000000, 0.000000000000000000, -0.000000000000000000 ) ) ;
#12573=CARTESIAN_POINT ( 'NONE',  ( 31.00000000000003553, 19.00000000000000000, 25.99999999999999645 ) ) ;
#12579=CARTESIAN_POINT ( 'NONE',  ( 40.00000000000000711, 19.00000000000000000, -26.00000000000000355 ) ) ;
#12596=DIRECTION ( 'NONE',  ( 0.000000000000000000, 1.000000000000000000, 0.000000000000000000 ) ) ;
#12601=DIRECTION ( 'NONE',  ( 0.000000000000000000, 0.000000000000000000, -1.000000000000000000 ) ) ;
#12632=DIRECTION ( 'NONE',  ( 0.000000000000000000, 0.000000000000000000, -1.000000000000000000 ) ) ;
#12637=EDGE_CURVE ( 'NONE', #4318, #4133, #14766, .T. ) ;
#12643=ORIENTED_EDGE ( 'NONE', *, *, #13102, .F. ) ;
#12660=EDGE_CURVE ( 'NONE', #10621, #2722, #8144, .T. ) ;
#12672=DIRECTION ( 'NONE',  ( -0.000000000000000000, -1.000000000000000000, -0.000000000000000000 ) ) ;
#12678=EDGE_LOOP ( 'NONE', ( #15334, #1445, #4674, #14294 ) ) ;
#12682=DIRECTION ( 'NONE',  ( 1.000000000000000000, 0.000000000000000000, 0.000000000000000000 ) ) ;
#12691=VERTEX_POINT ( 'NONE', #9437 ) ;
#12696=CARTESIAN_POINT ( 'NONE',  ( -26.00000000000000000, 11.00000000000000000, -31.00000000000003908 ) ) ;
#12698=VERTEX_POINT ( 'NONE', #14846 ) ;
#12714=ORIENTED_EDGE ( 'NONE', *, *, #4876, .T. ) ;
#12738=CIRCLE ( 'NONE', #2595, 18.50000000000000000 ) ;
#12742=ORIENTED_EDGE ( 'NONE', *, *, #2291, .T. ) ;
#12744=DIRECTION ( 'NONE',  ( -0.000000000000000000, -1.000000000000000000, -0.000000000000000000 ) ) ;
#12750=CARTESIAN_POINT ( 'NONE',  ( -31.00000000000000000, 8.000000000000000000, -31.00000000000000000 ) ) ;
#12755=ORIENTED_EDGE ( 'NONE', *, *, #8365, .T. ) ;
#12756=LINE ( 'NONE', #6457, #4409 ) ;
#12765=EDGE_CURVE ( 'NONE', #12691, #16882, #16461, .T. ) ;
#12773=CARTESIAN_POINT ( 'NONE',  ( -26.00000000000000000, 19.00000000000000000, -31.00000000000003908 ) ) ;
#12786=LINE ( 'NONE', #8671, #5268 ) ;
#12795=ORIENTED_EDGE ( 'NONE', *, *, #5181, .T. ) ;
#12803=DIRECTION ( 'NONE',  ( -0.000000000000000000, -1.000000000000000000, -0.000000000000000000 ) ) ;
#12811=CARTESIAN_POINT ( 'NONE',  ( 31.00000000000000000, 11.00000000000000000, 30.99999999999999289 ) ) ;
#12818=VERTEX_POINT ( 'NONE', #8572 ) ;
#12819=FACE_OUTER_BOUND ( 'NONE', #9470, .T. ) ;
#12824=DIRECTION ( 'NONE',  ( 0.000000000000000000, 1.000000000000000000, 0.000000000000000000 ) ) ;
#12833=ORIENTED_EDGE ( 'NONE', *, *, #6661, .T. ) ;
#12841=DIRECTION ( 'NONE',  ( -0.000000000000000000, 1.000000000000000000, -0.000000000000000000 ) ) ;
#12852=CARTESIAN_POINT ( 'NONE',  ( 31.81980515339464333, 0.000000000000000000, -35.11980515339463693 ) ) ;
#12853=CARTESIAN_POINT ( 'NONE',  ( 26.00000000000000355, 11.00000000000000000, -31.00000000000004263 ) ) ;
#12855=DIRECTION ( 'NONE',  ( 0.000000000000000000, 0.000000000000000000, 1.000000000000000000 ) ) ;
#12859=CARTESIAN_POINT ( 'NONE',  ( -26.00000000000000000, 19.00000000000000000, -40.00000000000000711 ) ) ;
#12904=LINE ( 'NONE', #9043, #7224 ) ;
#12927=DIRECTION ( 'NONE',  ( 0.000000000000000000, -1.000000000000000000, 0.000000000000000000 ) ) ;
#12946=LINE ( 'NONE', #1024, #10493 ) ;
#12948=DIRECTION ( 'NONE',  ( 0.000000000000000000, 0.000000000000000000, -1.000000000000000000 ) ) ;
#12953=LINE ( 'NONE', #1191, #2700 ) ;
#12957=VECTOR ( 'NONE', #13409, 1000.000000000000000 ) ;
#12964=VECTOR ( 'NONE', #13211, 1000.000000000000000 ) ;
#12974=DIRECTION ( 'NONE',  ( -0.000000000000000000, -1.000000000000000000, -0.000000000000000000 ) ) ;
#13011=CARTESIAN_POINT ( 'NONE',  ( -34.99999999999996447, 0.000000000000000000, -40.00000000000000711 ) ) ;
#13043=VECTOR ( 'NONE', #1687, 1000.000000000000000 ) ;
#13050=ORIENTED_EDGE ( 'NONE', *, *, #2015, .F. ) ;
#13053=CYLINDRICAL_SURFACE ( 'NONE', #16118, 4.999999999999997335 ) ;
#13054=CARTESIAN_POINT ( 'NONE',  ( 35.00000000000000711, 19.00000000000000000, 20.99999999999999289 ) ) ;
#13057=VECTOR ( 'NONE', #4821, 1000.000000000000000 ) ;
#13061=EDGE_CURVE ( 'NONE', #10961, #6790, #11994, .T. ) ;
#13072=CARTESIAN_POINT ( 'NONE',  ( -35.00000000000000000, 8.000000000000000000, -21.00000000000000000 ) ) ;
#13075=CARTESIAN_POINT ( 'NONE',  ( -31.00000000000000000, 8.000000000000000000, 30.99999999999999289 ) ) ;
#13082=ADVANCED_FACE ( 'NONE', ( #11814 ), #7939, .F. ) ;
#13083=EDGE_CURVE ( 'NONE', #8729, #16870, #4353, .T. ) ;
#13091=CIRCLE ( 'NONE', #7316, 4.999999999999997335 ) ;
#13100=EDGE_CURVE ( 'NONE', #3987, #1755, #147, .T. ) ;
#13102=EDGE_CURVE ( 'NONE', #16324, #5761, #8122, .T. ) ;
#13103=ORIENTED_EDGE ( 'NONE', *, *, #16531, .F. ) ;
#13117=VECTOR ( 'NONE', #16184, 1000.000000000000000 ) ;
#13118=FACE_OUTER_BOUND ( 'NONE', #16370, .T. ) ;
#13126=AXIS2_PLACEMENT_3D ( 'NONE', #316, #6985, #3058 ) ;
#13127=CARTESIAN_POINT ( 'NONE',  ( 21.00000000000000000, 8.000000000000000000, -35.00000000000000711 ) ) ;
#13135=FACE_OUTER_BOUND ( 'NONE', #5764, .T. ) ;
#13144=FACE_OUTER_BOUND ( 'NONE', #10581, .T. ) ;
#13165=DIRECTION ( 'NONE',  ( -1.000000000000000000, 0.000000000000000000, 0.000000000000000000 ) ) ;
#13191=CARTESIAN_POINT ( 'NONE',  ( -31.81980515339462912, 0.000000000000000000, 28.51980515339464972 ) ) ;
#13211=DIRECTION ( 'NONE',  ( -0.000000000000000000, -0.000000000000000000, 1.000000000000000000 ) ) ;
#13212=CARTESIAN_POINT ( 'NONE',  ( 35.00000000000000711, 11.00000000000000000, 35.00000000000000711 ) ) ;
#13213=VERTEX_POINT ( 'NONE', #5794 ) ;
#13217=ORIENTED_EDGE ( 'NONE', *, *, #686, .F. ) ;
#13221=ORIENTED_EDGE ( 'NONE', *, *, #12765, .F. ) ;
#13222=AXIS2_PLACEMENT_3D ( 'NONE', #16901, #1364, #9096 ) ;
#13233=DIRECTION ( 'NONE',  ( 0.000000000000000000, 0.000000000000000000, -1.000000000000000000 ) ) ;
#13249=VECTOR ( 'NONE', #570, 1000.000000000000000 ) ;
#13253=AXIS2_PLACEMENT_3D ( 'NONE', #6151, #12601, #845 ) ;
#13255=CARTESIAN_POINT ( 'NONE',  ( -26.00000000000000000, 11.00000000000000000, -40.00000000000000711 ) ) ;
#13271=ORIENTED_EDGE ( 'NONE', *, *, #15504, .T. ) ;
#13293=EDGE_CURVE ( 'NONE', #10521, #4853, #11527, .T. ) ;
#13297=ORIENTED_EDGE ( 'NONE', *, *, #11904, .F. ) ;
#13310=DIRECTION ( 'NONE',  ( 0.000000000000000000, 0.000000000000000000, 1.000000000000000000 ) ) ;
#13312=CARTESIAN_POINT ( 'NONE',  ( 31.81980515339464333, 11.00000000000000000, -31.81980515339463622 ) ) ;
#13318=FACE_OUTER_BOUND ( 'NONE', #12285, .T. ) ;
#13321=DIRECTION ( 'NONE',  ( -0.000000000000000000, -1.000000000000000000, -0.000000000000000000 ) ) ;
#13327=ORIENTED_EDGE ( 'NONE', *, *, #6592, .F. ) ;
#13330=DIRECTION ( 'NONE',  ( 0.000000000000000000, 1.000000000000000000, 0.000000000000000000 ) ) ;
#13336=VECTOR ( 'NONE', #1589, 1000.000000000000000 ) ;
#13347=FACE_OUTER_BOUND ( 'NONE', #6673, .T. ) ;
#13366=DIRECTION ( 'NONE',  ( -1.000000000000000000, -0.000000000000000000, -0.000000000000000000 ) ) ;
#13369=EDGE_CURVE ( 'NONE', #2442, #8649, #7644, .T. ) ;
#13372=DIRECTION ( 'NONE',  ( 0.000000000000000000, 0.000000000000000000, -1.000000000000000000 ) ) ;
#13378=DIRECTION ( 'NONE',  ( 0.000000000000000000, 0.000000000000000000, 1.000000000000000000 ) ) ;
#13379=DIRECTION ( 'NONE',  ( 0.000000000000000000, 1.000000000000000000, 0.000000000000000000 ) ) ;
#13409=DIRECTION ( 'NONE',  ( -1.000000000000000000, -0.000000000000000000, -0.000000000000000000 ) ) ;
#13414=DIRECTION ( 'NONE',  ( 0.000000000000000000, 0.000000000000000000, -1.000000000000000000 ) ) ;
#13432=ORIENTED_EDGE ( 'NONE', *, *, #5536, .T. ) ;
#13438=VERTEX_POINT ( 'NONE', #1900 ) ;
#13440=CARTESIAN_POINT ( 'NONE',  ( -20.99999999999999645, 19.00000000000000000, 35.00000000000001421 ) ) ;
#13441=VERTEX_POINT ( 'NONE', #5934 ) ;
#13447=CARTESIAN_POINT ( 'NONE',  ( 31.81980515339464333, 11.00000000000000000, 31.81980515339463622 ) ) ;
#13462=AXIS2_PLACEMENT_3D ( 'NONE', #10398, #8858, #7809 ) ;
#13490=EDGE_CURVE ( 'NONE', #10460, #14475, #7213, .T. ) ;
#13503=CARTESIAN_POINT ( 'NONE',  ( 26.00000000000000000, 11.00000000000000000, 31.00000000000003197 ) ) ;
#13517=DIRECTION ( 'NONE',  ( 1.000000000000000000, 0.000000000000000000, 0.000000000000000000 ) ) ;
#13519=LINE ( 'NONE', #13607, #2551 ) ;
#13522=CIRCLE ( 'NONE', #9120, 9.999999999999998224 ) ;
#13536=EDGE_CURVE ( 'NONE', #14008, #16924, #8066, .T. ) ;
#13540=DIRECTION ( 'NONE',  ( 0.000000000000000000, 0.000000000000000000, -1.000000000000000000 ) ) ;
#13554=DIRECTION ( 'NONE',  ( -1.000000000000000000, 0.000000000000000000, 0.000000000000000000 ) ) ;
#13567=VECTOR ( 'NONE', #10070, 1000.000000000000000 ) ;
#13570=CIRCLE ( 'NONE', #11355, 4.999999999999997335 ) ;
#13571=DIRECTION ( 'NONE',  ( 0.000000000000000000, 1.000000000000000000, 0.000000000000000000 ) ) ;
#13577=FILL_AREA_STYLE_COLOUR ( '', #10226 ) ;
#13579=AXIS2_PLACEMENT_3D ( 'NONE', #9468, #10837, #1823 ) ;
#13607=CARTESIAN_POINT ( 'NONE',  ( 21.00000000000000000, 8.000000000000000000, -31.00000000000003908 ) ) ;
#13623=DIRECTION ( 'NONE',  ( 0.000000000000000000, 0.000000000000000000, 1.000000000000000000 ) ) ;
#13638=CARTESIAN_POINT ( 'NONE',  ( 31.00000000000003553, 19.00000000000000000, 25.99999999999999645 ) ) ;
#13652=AXIS2_PLACEMENT_3D ( 'NONE', #7493, #4922, #1065 ) ;
#13660=VERTEX_POINT ( 'NONE', #6939 ) ;
#13670=CARTESIAN_POINT ( 'NONE',  ( -31.81980515339462912, 11.00000000000000000, -31.81980515339465043 ) ) ;
#13675=SHAPE_DEFINITION_REPRESENTATION ( #3828, #11211 ) ;
#13682=EDGE_CURVE ( 'NONE', #14008, #13213, #9709, .T. ) ;
#13695=ORIENTED_EDGE ( 'NONE', *, *, #598, .F. ) ;
#13697=LINE ( 'NONE', #12573, #861 ) ;
#13701=VECTOR ( 'NONE', #9414, 1000.000000000000000 ) ;
#13705=DIRECTION ( 'NONE',  ( -0.000000000000000000, -1.000000000000000000, -0.000000000000000000 ) ) ;
#13710=CARTESIAN_POINT ( 'NONE',  ( 31.00000000000000000, 19.00000000000000000, -21.00000000000000355 ) ) ;
#13740=PLANE ( 'NONE',  #909 ) ;
#13744=CARTESIAN_POINT ( 'NONE',  ( -35.00000000000000000, 8.000000000000000000, 20.99999999999999289 ) ) ;
#13751=EDGE_CURVE ( 'NONE', #4924, #1561, #4387, .T. ) ;
#13768=ORIENTED_EDGE ( 'NONE', *, *, #2151, .F. ) ;
#13794=LINE ( 'NONE', #2020, #6430 ) ;
#13837=DIRECTION ( 'NONE',  ( -1.000000000000000000, 0.000000000000000000, 3.854941057726251409E-16 ) ) ;
#13844=AXIS2_PLACEMENT_3D ( 'NONE', #7549, #12974, #961 ) ;
#13846=ORIENTED_EDGE ( 'NONE', *, *, #12637, .T. ) ;
#13850=ORIENTED_EDGE ( 'NONE', *, *, #8705, .T. ) ;
#13855=LINE ( 'NONE', #12390, #3937 ) ;
#13859=VERTEX_POINT ( 'NONE', #15606 ) ;
#13865=DIRECTION ( 'NONE',  ( 0.000000000000000000, 0.000000000000000000, -1.000000000000000000 ) ) ;
#13871=ORIENTED_EDGE ( 'NONE', *, *, #14537, .F. ) ;
#13878=VERTEX_POINT ( 'NONE', #3594 ) ;
#13889=ADVANCED_FACE ( 'NONE', ( #14160 ), #14317, .T. ) ;
#13894=CARTESIAN_POINT ( 'NONE',  ( -31.81980515339462912, 0.000000000000000000, 31.81980515339465043 ) ) ;
#13902=EDGE_CURVE ( 'NONE', #8973, #12698, #7611, .T. ) ;
#13908=CARTESIAN_POINT ( 'NONE',  ( -26.00000000000000000, 19.00000000000000000, -31.00000000000003908 ) ) ;
#13931=EDGE_CURVE ( 'NONE', #5761, #5602, #15685, .T. ) ;
#13938=CARTESIAN_POINT ( 'NONE',  ( -20.99999999999999645, 19.00000000000000000, -31.00000000000003908 ) ) ;
#13941=AXIS2_PLACEMENT_3D ( 'NONE', #14121, #8634, #13865 ) ;
#13957=CARTESIAN_POINT ( 'NONE',  ( 31.81980515339464333, 11.00000000000000000, 35.11980515339463693 ) ) ;
#13960=DIRECTION ( 'NONE',  ( -0.000000000000000000, -1.000000000000000000, -0.000000000000000000 ) ) ;
#13963=VERTEX_POINT ( 'NONE', #7009 ) ;
#13964=CARTESIAN_POINT ( 'NONE',  ( -31.00000000000000000, 11.00000000000000000, 30.99999999999999289 ) ) ;
#13978=AXIS2_PLACEMENT_3D ( 'NONE', #8419, #16391, #9954 ) ;
#13986=AXIS2_PLACEMENT_3D ( 'NONE', #11480, #10372, #14156 ) ;
#13999=CARTESIAN_POINT ( 'NONE',  ( 0.000000000000000000, 19.00100000000000122, 0.000000000000000000 ) ) ;
#14008=VERTEX_POINT ( 'NONE', #499 ) ;
#14012=VERTEX_POINT ( 'NONE', #4768 ) ;
#14025=EDGE_CURVE ( 'NONE', #4477, #1411, #4438, .T. ) ;
#14060=CARTESIAN_POINT ( 'NONE',  ( -31.81980515339462912, 8.000000000000000000, 31.81980515339465043 ) ) ;
#14086=AXIS2_PLACEMENT_3D ( 'NONE', #7718, #16830, #8947 ) ;
#14087=CARTESIAN_POINT ( 'NONE',  ( -39.99999999999999289, 11.00000000000000000, 25.99999999999999645 ) ) ;
#14089=CIRCLE ( 'NONE', #5295, 35.00000000000000711 ) ;
#14091=DIRECTION ( 'NONE',  ( -0.000000000000000000, -1.000000000000000000, -0.000000000000000000 ) ) ;
#14100=DIRECTION ( 'NONE',  ( 0.000000000000000000, 0.000000000000000000, -1.000000000000000000 ) ) ;
#14104=EDGE_CURVE ( 'NONE', #4853, #10521, #1962, .T. ) ;
#14113=ORIENTED_EDGE ( 'NONE', *, *, #6223, .T. ) ;
#14121=CARTESIAN_POINT ( 'NONE',  ( 35.00000000000000711, 0.000000000000000000, -35.00000000000000711 ) ) ;
#14139=CARTESIAN_POINT ( 'NONE',  ( 0.000000000000000000, -3.000000000000000000, 0.000000000000000000 ) ) ;
#14146=CARTESIAN_POINT ( 'NONE',  ( -31.81980515339462912, 8.000000000000000000, 31.81980515339465043 ) ) ;
#14156=DIRECTION ( 'NONE',  ( 1.000000000000000000, 0.000000000000000000, -0.000000000000000000 ) ) ;
#14160=FACE_OUTER_BOUND ( 'NONE', #454, .T. ) ;
#14171=ORIENTED_EDGE ( 'NONE', *, *, #13902, .F. ) ;
#14173=VECTOR ( 'NONE', #3127, 1000.000000000000000 ) ;
#14178=FACE_BOUND ( 'NONE', #3714, .T. ) ;
#14186=LINE ( 'NONE', #2487, #10709 ) ;
#14217=VECTOR ( 'NONE', #10917, 1000.000000000000000 ) ;
#14218=EDGE_LOOP ( 'NONE', ( #10844, #8960, #3883, #9552 ) ) ;
#14222=CARTESIAN_POINT ( 'NONE',  ( -26.00000000000000355, 19.00000000000000000, 31.00000000000003197 ) ) ;
#14239=EDGE_CURVE ( 'NONE', #747, #13878, #14737, .T. ) ;
#14242=ADVANCED_FACE ( 'NONE', ( #14478 ), #224, .T. ) ;
#14248=ORIENTED_EDGE ( 'NONE', *, *, #3732, .T. ) ;
#14262=FACE_OUTER_BOUND ( 'NONE', #5856, .T. ) ;
#14267=ORIENTED_EDGE ( 'NONE', *, *, #9600, .T. ) ;
#14270=DIRECTION ( 'NONE',  ( 0.000000000000000000, 1.000000000000000000, 0.000000000000000000 ) ) ;
#14293=PLANE ( 'NONE',  #5904 ) ;
#14294=ORIENTED_EDGE ( 'NONE', *, *, #4255, .T. ) ;
#14300=ORIENTED_EDGE ( 'NONE', *, *, #6361, .T. ) ;
#14306=VECTOR ( 'NONE', #9690, 1000.000000000000000 ) ;
#14317=PLANE ( 'NONE',  #3622 ) ;
#14331=CYLINDRICAL_SURFACE ( 'NONE', #1694, 4.999999999999997335 ) ;
#14332=EDGE_CURVE ( 'NONE', #3447, #10304, #8381, .T. ) ;
#14347=CARTESIAN_POINT ( 'NONE',  ( 31.00000000000000000, 19.00000000000000000, 30.99999999999999289 ) ) ;
#14359=DIRECTION ( 'NONE',  ( -0.000000000000000000, -1.000000000000000000, -0.000000000000000000 ) ) ;
#14368=DIRECTION ( 'NONE',  ( 0.000000000000000000, 0.000000000000000000, 1.000000000000000000 ) ) ;
#14373=AXIS2_PLACEMENT_3D ( 'NONE', #14622, #2682, #119 ) ;
#14414=AXIS2_PLACEMENT_3D ( 'NONE', #15529, #3767, #9003 ) ;
#14425=VECTOR ( 'NONE', #7310, 1000.000000000000000 ) ;
#14437=DIRECTION ( 'NONE',  ( 1.000000000000000000, 0.000000000000000000, -0.000000000000000000 ) ) ;
#14439=DIRECTION ( 'NONE',  ( -3.854941057726249437E-16, 0.000000000000000000, -1.000000000000000000 ) ) ;
#14445=EDGE_LOOP ( 'NONE', ( #3366, #13297, #6802, #14976 ) ) ;
#14450=ADVANCED_FACE ( 'NONE', ( #11363 ), #6505, .F. ) ;
#14457=ADVANCED_FACE ( 'NONE', ( #2170 ), #4834, .T. ) ;
#14475=VERTEX_POINT ( 'NONE', #5317 ) ;
#14478=FACE_OUTER_BOUND ( 'NONE', #3782, .T. ) ;
#14480=MANIFOLD_SOLID_BREP ( 'Boss-Extrude4', #15671 ) ;
#14481=LINE ( 'NONE', #14222, #6591 ) ;
#14485=DIRECTION ( 'NONE',  ( -0.000000000000000000, -1.000000000000000000, -0.000000000000000000 ) ) ;
#14526=EDGE_CURVE ( 'NONE', #12218, #15841, #602, .T. ) ;
#14534=DIRECTION ( 'NONE',  ( -1.000000000000000000, 0.000000000000000000, 0.000000000000000000 ) ) ;
#14537=EDGE_CURVE ( 'NONE', #12698, #7827, #4386, .T. ) ;
#14578=CARTESIAN_POINT ( 'NONE',  ( 2.265596578422603396E-15, 19.00100000000000122, 18.50000000000000000 ) ) ;
#14583=EDGE_CURVE ( 'NONE', #3282, #4422, #12786, .T. ) ;
#14593=ORIENTED_EDGE ( 'NONE', *, *, #5790, .F. ) ;
#14595=DIRECTION ( 'NONE',  ( 0.000000000000000000, 0.000000000000000000, 1.000000000000000000 ) ) ;
#14604=CARTESIAN_POINT ( 'NONE',  ( -31.00000000000003197, 19.00000000000000000, -26.00000000000000355 ) ) ;
#14608=CYLINDRICAL_SURFACE ( 'NONE', #6455, 5.000000000000000888 ) ;
#14613=LINE ( 'NONE', #13503, #10550 ) ;
#14614=VERTEX_POINT ( 'NONE', #2128 ) ;
#14622=CARTESIAN_POINT ( 'NONE',  ( -31.00000000000000000, 19.00000000000000000, 30.99999999999999289 ) ) ;
#14631=VECTOR ( 'NONE', #16861, 1000.000000000000000 ) ;
#14645=ORIENTED_EDGE ( 'NONE', *, *, #5598, .T. ) ;
#14648=ORIENTED_EDGE ( 'NONE', *, *, #14526, .T. ) ;
#14659=CARTESIAN_POINT ( 'NONE',  ( 40.00000000000000711, 8.000000000000000000, 34.99999999999997868 ) ) ;
#14674=EDGE_CURVE ( 'NONE', #4133, #10494, #11318, .T. ) ;
#14680=AXIS2_PLACEMENT_3D ( 'NONE', #14347, #8163, #13414 ) ;
#14694=PRESENTATION_STYLE_ASSIGNMENT (( #10910 ) ) ;
#14697=DIRECTION ( 'NONE',  ( 0.000000000000000000, 0.000000000000000000, 1.000000000000000000 ) ) ;
#14712=ORIENTED_EDGE ( 'NONE', *, *, #2697, .F. ) ;
#14717=PLANE ( 'NONE',  #16766 ) ;
#14718=CYLINDRICAL_SURFACE ( 'NONE', #14373, 4.999999999999997335 ) ;
#14737=LINE ( 'NONE', #5262, #3088 ) ;
#14739=FACE_BOUND ( 'NONE', #14803, .T. ) ;
#14743=FACE_OUTER_BOUND ( 'NONE', #1833, .T. ) ;
#14747=EDGE_CURVE ( 'NONE', #13660, #394, #4023, .T. ) ;
#14753=ORIENTED_EDGE ( 'NONE', *, *, #615, .F. ) ;
#14756=DIRECTION ( 'NONE',  ( 0.000000000000000000, 0.000000000000000000, -1.000000000000000000 ) ) ;
#14766=LINE ( 'NONE', #10714, #9888 ) ;
#14771=DIRECTION ( 'NONE',  ( 0.000000000000000000, 0.000000000000000000, 1.000000000000000000 ) ) ;
#14777=EDGE_CURVE ( 'NONE', #9952, #2442, #12946, .T. ) ;
#14790=ORIENTED_EDGE ( 'NONE', *, *, #3116, .T. ) ;
#14802=CARTESIAN_POINT ( 'NONE',  ( 2.265596578422603396E-15, -3.000000000000000000, 18.50000000000000000 ) ) ;
#14803=EDGE_LOOP ( 'NONE', ( #1624, #2211 ) ) ;
#14824=DIRECTION ( 'NONE',  ( 0.000000000000000000, 0.000000000000000000, 1.000000000000000000 ) ) ;
#14826=CARTESIAN_POINT ( 'NONE',  ( -34.99999999999996447, 11.00000000000000000, 40.00000000000000711 ) ) ;
#14829=VECTOR ( 'NONE', #3931, 1000.000000000000000 ) ;
#14841=ORIENTED_EDGE ( 'NONE', *, *, #14674, .F. ) ;
#14846=CARTESIAN_POINT ( 'NONE',  ( 40.00000000000000711, 19.00000000000000000, 25.99999999999999645 ) ) ;
#14848=CARTESIAN_POINT ( 'NONE',  ( 31.81980515339464333, 8.000000000000000000, 31.81980515339463622 ) ) ;
#14893=VECTOR ( 'NONE', #10959, 1000.000000000000000 ) ;
#14917=CIRCLE ( 'NONE', #11616, 10.00000000000000178 ) ;
#14936=CYLINDRICAL_SURFACE ( 'NONE', #9923, 3.299999999999997158 ) ;
#14950=CARTESIAN_POINT ( 'NONE',  ( -31.00000000000006395, 19.00000000000000000, 20.99999999999998934 ) ) ;
#14951=ORIENTED_EDGE ( 'NONE', *, *, #13931, .T. ) ;
#14953=CARTESIAN_POINT ( 'NONE',  ( 4.286263797015737285E-15, -3.000000000000000000, -35.00000000000000711 ) ) ;
#14964=ADVANCED_FACE ( 'NONE', ( #328 ), #12006, .T. ) ;
#14974=FACE_BOUND ( 'NONE', #9033, .T. ) ;
#14976=ORIENTED_EDGE ( 'NONE', *, *, #2151, .T. ) ;
#15019=DIRECTION ( 'NONE',  ( 0.000000000000000000, 0.000000000000000000, -1.000000000000000000 ) ) ;
#15025=ORIENTED_EDGE ( 'NONE', *, *, #7489, .T. ) ;
#15027=ADVANCED_FACE ( 'NONE', ( #1944 ), #16624, .T. ) ;
#15031=LINE ( 'NONE', #13744, #518 ) ;
#15049=ORIENTED_EDGE ( 'NONE', *, *, #13102, .T. ) ;
#15061=CARTESIAN_POINT ( 'NONE',  ( -26.00000000000000000, 19.00000000000000000, -40.00000000000000711 ) ) ;
#15062=DIRECTION ( 'NONE',  ( 0.000000000000000000, 0.000000000000000000, -1.000000000000000000 ) ) ;
#15064=LINE ( 'NONE', #5711, #236 ) ;
#15066=ADVANCED_FACE ( 'NONE', ( #5806, #3247 ), #7088, .T. ) ;
#15072=ORIENTED_EDGE ( 'NONE', *, *, #4637, .F. ) ;
#15083=CARTESIAN_POINT ( 'NONE',  ( 31.00000000000000000, 11.00000000000000000, -31.00000000000000355 ) ) ;
#15084=VERTEX_POINT ( 'NONE', #4533 ) ;
#15110=ORIENTED_EDGE ( 'NONE', *, *, #12660, .T. ) ;
#15142=VERTEX_POINT ( 'NONE', #5107 ) ;
#15155=CARTESIAN_POINT ( 'NONE',  ( 40.00000000000000711, 0.000000000000000000, 34.99999999999997868 ) ) ;
#15160=EDGE_LOOP ( 'NONE', ( #11415, #7317, #10132, #3808 ) ) ;
#15161=ORIENTED_EDGE ( 'NONE', *, *, #13751, .T. ) ;
#15173=DIRECTION ( 'NONE',  ( 0.000000000000000000, 1.000000000000000000, 0.000000000000000000 ) ) ;
#15182=DIRECTION ( 'NONE',  ( 0.000000000000000000, 1.000000000000000000, 0.000000000000000000 ) ) ;
#15199=( GEOMETRIC_REPRESENTATION_CONTEXT ( 3 ) GLOBAL_UNCERTAINTY_ASSIGNED_CONTEXT ( ( #7595 ) ) GLOBAL_UNIT_ASSIGNED_CONTEXT ( ( #11678, #3703, #15794 ) ) REPRESENTATION_CONTEXT ( 'NONE', 'WORKASPACE' ) );
#15206=DIRECTION ( 'NONE',  ( 1.000000000000000000, 0.000000000000000000, -0.000000000000000000 ) ) ;
#15217=DIRECTION ( 'NONE',  ( 1.000000000000000000, 0.000000000000000000, 0.000000000000000000 ) ) ;
#15250=CIRCLE ( 'NONE', #4548, 3.299999999999997158 ) ;
#15256=CARTESIAN_POINT ( 'NONE',  ( -31.81980515339462912, 8.000000000000000000, 28.51980515339464972 ) ) ;
#15267=CARTESIAN_POINT ( 'NONE',  ( -20.99999999999999645, 8.000000000000000000, 35.00000000000001421 ) ) ;
#15268=CARTESIAN_POINT ( 'NONE',  ( -31.81980515339462912, 11.00000000000000000, -31.81980515339465043 ) ) ;
#15282=CIRCLE ( 'NONE', #7863, 3.300000000000004263 ) ;
#15284=ORIENTED_EDGE ( 'NONE', *, *, #4380, .F. ) ;
#15300=PRODUCT_CONTEXT ( 'NONE', #9746, 'mechanical' ) ;
#15304=CARTESIAN_POINT ( 'NONE',  ( -34.99999999999996447, 0.000000000000000000, -40.00000000000000711 ) ) ;
#15308=CARTESIAN_POINT ( 'NONE',  ( 21.00000000000000000, 19.00000000000000000, 35.00000000000001421 ) ) ;
#15317=ORIENTED_EDGE ( 'NONE', *, *, #12660, .F. ) ;
#15334=ORIENTED_EDGE ( 'NONE', *, *, #9600, .F. ) ;
#15379=ADVANCED_FACE ( 'NONE', ( #14739, #1772 ), #5446, .T. ) ;
#15388=EDGE_LOOP ( 'NONE', ( #7817, #14267, #2863, #1055 ) ) ;
#15411=AXIS2_PLACEMENT_3D ( 'NONE', #1541, #6934, #5658 ) ;
#15434=ORIENTED_EDGE ( 'NONE', *, *, #2246, .F. ) ;
#15435=CARTESIAN_POINT ( 'NONE',  ( -26.00000000000000355, 19.00000000000000000, 31.00000000000003197 ) ) ;
#15454=ORIENTED_EDGE ( 'NONE', *, *, #2697, .T. ) ;
#15463=CIRCLE ( 'NONE', #10798, 4.999999999999997335 ) ;
#15470=DIRECTION ( 'NONE',  ( 0.000000000000000000, -0.000000000000000000, 1.000000000000000000 ) ) ;
#15478=ORIENTED_EDGE ( 'NONE', *, *, #245, .F. ) ;
#15482=PLANE ( 'NONE',  #8635 ) ;
#15486=ORIENTED_EDGE ( 'NONE', *, *, #2457, .T. ) ;
#15491=ADVANCED_FACE ( 'NONE', ( #4513 ), #16432, .T. ) ;
#15492=ORIENTED_EDGE ( 'NONE', *, *, #12126, .T. ) ;
#15498=CYLINDRICAL_SURFACE ( 'NONE', #6941, 10.00000000000000178 ) ;
#15500=ORIENTED_EDGE ( 'NONE', *, *, #10367, .F. ) ;
#15501=DIRECTION ( 'NONE',  ( -0.000000000000000000, -1.000000000000000000, -0.000000000000000000 ) ) ;
#15504=EDGE_CURVE ( 'NONE', #10620, #2369, #15463, .T. ) ;
#15511=CIRCLE ( 'NONE', #1805, 3.299999999999997158 ) ;
#15513=ORIENTED_EDGE ( 'NONE', *, *, #4003, .F. ) ;
#15529=CARTESIAN_POINT ( 'NONE',  ( 31.00000000000000000, 11.00000000000000000, 30.99999999999999289 ) ) ;
#15531=DIRECTION ( 'NONE',  ( 1.000000000000000000, 0.000000000000000000, 0.000000000000000000 ) ) ;
#15543=VECTOR ( 'NONE', #12682, 1000.000000000000000 ) ;
#15544=LINE ( 'NONE', #9094, #12352 ) ;
#15559=CARTESIAN_POINT ( 'NONE',  ( 21.00000000000000000, 8.000000000000000000, 35.00000000000001421 ) ) ;
#15578=CARTESIAN_POINT ( 'NONE',  ( 0.000000000000000000, -3.000000000000000000, 0.000000000000000000 ) ) ;
#15583=ADVANCED_FACE ( 'NONE', ( #641 ), #5876, .T. ) ;
#15589=EDGE_CURVE ( 'NONE', #4239, #12007, #2004, .T. ) ;
#15606=CARTESIAN_POINT ( 'NONE',  ( 40.00000000000000711, 11.00000000000000000, -34.99999999999997868 ) ) ;
#15620=CARTESIAN_POINT ( 'NONE',  ( -34.99999999999996447, 8.000000000000000000, 40.00000000000000711 ) ) ;
#15624=EDGE_CURVE ( 'NONE', #13859, #903, #12904, .T. ) ;
#15628=DIRECTION ( 'NONE',  ( -0.000000000000000000, -1.000000000000000000, -0.000000000000000000 ) ) ;
#15629=PLANE ( 'NONE',  #12466 ) ;
#15637=DIRECTION ( 'NONE',  ( -0.000000000000000000, -1.000000000000000000, -0.000000000000000000 ) ) ;
#15652=FACE_BOUND ( 'NONE', #2240, .T. ) ;
#15671=CLOSED_SHELL ( 'NONE', ( #8351, #5347, #487, #14450, #4439, #10892, #10472, #14457, #1129, #4174, #6764, #37, #13082, #8618, #16657, #16020, #2303, #161, #16607, #8015, #8219, #11082, #8462, #16234, #16023, #15804, #1230, #7703, #9412, #3579, #8772, #6997, #2578, #16743, #15027, #11279, #15491, #13889, #14242, #4084, #16236, #15583, #10544, #14964, #16278, #11340, #7092, #4056, #11778, #1310, #15379, #16660, #15066, #9369, #5270, #4469 ) ) ;
#15673=DIRECTION ( 'NONE',  ( 0.000000000000000000, 0.000000000000000000, -1.000000000000000000 ) ) ;
#15685=LINE ( 'NONE', #1267, #12398 ) ;
#15690=ORIENTED_EDGE ( 'NONE', *, *, #1021, .T. ) ;
#15698=CARTESIAN_POINT ( 'NONE',  ( -34.99999999999999289, 8.000000000000000000, 35.00000000000000711 ) ) ;
#15712=VERTEX_POINT ( 'NONE', #14802 ) ;
#15746=ORIENTED_EDGE ( 'NONE', *, *, #8456, .F. ) ;
#15747=EDGE_CURVE ( 'NONE', #10494, #10121, #6713, .T. ) ;
#15778=VECTOR ( 'NONE', #749, 1000.000000000000000 ) ;
#15794=( NAMED_UNIT ( * ) SI_UNIT ( $, .STERADIAN. ) SOLID_ANGLE_UNIT ( ) );
#15804=ADVANCED_FACE ( 'NONE', ( #3986 ), #14718, .F. ) ;
#15811=DIRECTION ( 'NONE',  ( 0.000000000000000000, 0.000000000000000000, -1.000000000000000000 ) ) ;
#15814=ORIENTED_EDGE ( 'NONE', *, *, #2986, .F. ) ;
#15816=CARTESIAN_POINT ( 'NONE',  ( -34.99999999999999289, 8.000000000000000000, -35.00000000000000711 ) ) ;
#15818=VECTOR ( 'NONE', #15908, 1000.000000000000000 ) ;
#15824=CARTESIAN_POINT ( 'NONE',  ( -40.00000000000000000, 19.00000000000000000, -26.00000000000000355 ) ) ;
#15841=VERTEX_POINT ( 'NONE', #15824 ) ;
#15859=ORIENTED_EDGE ( 'NONE', *, *, #15951, .T. ) ;
#15876=AXIS2_PLACEMENT_3D ( 'NONE', #12750, #3646, #7575 ) ;
#15898=FACE_BOUND ( 'NONE', #6988, .T. ) ;
#15906=DIRECTION ( 'NONE',  ( 1.000000000000000000, 0.000000000000000000, 0.000000000000000000 ) ) ;
#15908=DIRECTION ( 'NONE',  ( 1.000000000000000000, 0.000000000000000000, 0.000000000000000000 ) ) ;
#15909=LINE ( 'NONE', #11976, #10241 ) ;
#15910=ORIENTED_EDGE ( 'NONE', *, *, #6632, .F. ) ;
#15916=LINE ( 'NONE', #6726, #13336 ) ;
#15923=CARTESIAN_POINT ( 'NONE',  ( -20.99999999999999645, 19.00000000000000000, 35.00000000000001421 ) ) ;
#15926=ORIENTED_EDGE ( 'NONE', *, *, #259, .F. ) ;
#15933=CARTESIAN_POINT ( 'NONE',  ( 31.00000000000003553, 11.00000000000000000, -26.00000000000000355 ) ) ;
#15943=ORIENTED_EDGE ( 'NONE', *, *, #10574, .F. ) ;
#15951=EDGE_CURVE ( 'NONE', #11860, #15084, #1744, .T. ) ;
#15958=EDGE_CURVE ( 'NONE', #5994, #5602, #12473, .T. ) ;
#15965=ORIENTED_EDGE ( 'NONE', *, *, #596, .F. ) ;
#15986=ORIENTED_EDGE ( 'NONE', *, *, #1544, .T. ) ;
#15997=EDGE_CURVE ( 'NONE', #16035, #4239, #3685, .T. ) ;
#16020=ADVANCED_FACE ( 'NONE', ( #14262 ), #6179, .F. ) ;
#16023=ADVANCED_FACE ( 'NONE', ( #16742 ), #15629, .F. ) ;
#16026=LINE ( 'NONE', #14826, #9287 ) ;
#16035=VERTEX_POINT ( 'NONE', #11344 ) ;
#16056=DIRECTION ( 'NONE',  ( 0.000000000000000000, -0.000000000000000000, 1.000000000000000000 ) ) ;
#16059=EDGE_CURVE ( 'NONE', #7006, #8729, #2155, .T. ) ;
#16060=FILL_AREA_STYLE ('',( #13577 ) ) ;
#16061=ORIENTED_EDGE ( 'NONE', *, *, #5181, .F. ) ;
#16071=CIRCLE ( 'NONE', #16615, 3.299999999999997158 ) ;
#16074=FACE_OUTER_BOUND ( 'NONE', #9119, .T. ) ;
#16079=ORIENTED_EDGE ( 'NONE', *, *, #615, .T. ) ;
#16081=DIRECTION ( 'NONE',  ( 0.000000000000000000, -1.000000000000000000, 0.000000000000000000 ) ) ;
#16093=EDGE_CURVE ( 'NONE', #8783, #4809, #16588, .T. ) ;
#16118=AXIS2_PLACEMENT_3D ( 'NONE', #6582, #11837, #5899 ) ;
#16139=DIRECTION ( 'NONE',  ( 0.000000000000000000, 1.000000000000000000, 0.000000000000000000 ) ) ;
#16162=FACE_BOUND ( 'NONE', #8627, .T. ) ;
#16163=DIRECTION ( 'NONE',  ( 1.000000000000000000, 0.000000000000000000, 0.000000000000000000 ) ) ;
#16172=LINE ( 'NONE', #1281, #5128 ) ;
#16176=DIRECTION ( 'NONE',  ( 0.000000000000000000, 0.000000000000000000, 1.000000000000000000 ) ) ;
#16184=DIRECTION ( 'NONE',  ( 0.000000000000000000, 0.000000000000000000, -1.000000000000000000 ) ) ;
#16191=DIRECTION ( 'NONE',  ( 1.000000000000000000, 0.000000000000000000, 0.000000000000000000 ) ) ;
#16227=ORIENTED_EDGE ( 'NONE', *, *, #13931, .F. ) ;
#16232=ORIENTED_EDGE ( 'NONE', *, *, #13490, .F. ) ;
#16234=ADVANCED_FACE ( 'NONE', ( #3868 ), #11849, .F. ) ;
#16236=ADVANCED_FACE ( 'NONE', ( #9456 ), #2926, .T. ) ;
#16254=DIRECTION ( 'NONE',  ( -0.000000000000000000, -1.000000000000000000, 0.000000000000000000 ) ) ;
#16259=ORIENTED_EDGE ( 'NONE', *, *, #4685, .T. ) ;
#16263=( GEOMETRIC_REPRESENTATION_CONTEXT ( 3 ) GLOBAL_UNCERTAINTY_ASSIGNED_CONTEXT ( ( #11391 ) ) GLOBAL_UNIT_ASSIGNED_CONTEXT ( ( #6940, #5665, #1712 ) ) REPRESENTATION_CONTEXT ( 'NONE', 'WORKASPACE' ) );
#16278=ADVANCED_FACE ( 'NONE', ( #13144 ), #1373, .T. ) ;
#16308=CARTESIAN_POINT ( 'NONE',  ( -31.00000000000003553, 8.000000000000000000, -21.00000000000000000 ) ) ;
#16320=ORIENTED_EDGE ( 'NONE', *, *, #10148, .F. ) ;
#16322=CARTESIAN_POINT ( 'NONE',  ( 21.00000000000000000, 19.00000000000000000, -35.00000000000000711 ) ) ;
#16323=CARTESIAN_POINT ( 'NONE',  ( 40.00000000000000711, 11.00000000000000000, -26.00000000000000355 ) ) ;
#16324=VERTEX_POINT ( 'NONE', #3580 ) ;
#16357=DIRECTION ( 'NONE',  ( 0.000000000000000000, 0.000000000000000000, -1.000000000000000000 ) ) ;
#16360=VECTOR ( 'NONE', #12518, 1000.000000000000000 ) ;
#16369=EDGE_LOOP ( 'NONE', ( #3925, #7431, #10109, #11913 ) ) ;
#16370=EDGE_LOOP ( 'NONE', ( #5780, #13695, #11080, #15965 ) ) ;
#16391=DIRECTION ( 'NONE',  ( 0.000000000000000000, 1.000000000000000000, 0.000000000000000000 ) ) ;
#16410=CARTESIAN_POINT ( 'NONE',  ( 25.99999999999999645, 11.00000000000000000, 40.00000000000000711 ) ) ;
#16417=VECTOR ( 'NONE', #403, 1000.000000000000000 ) ;
#16427=ORIENTED_EDGE ( 'NONE', *, *, #15997, .F. ) ;
#16432=CYLINDRICAL_SURFACE ( 'NONE', #9715, 10.00000000000000178 ) ;
#16449=ORIENTED_EDGE ( 'NONE', *, *, #3415, .F. ) ;
#16451=CIRCLE ( 'NONE', #7386, 4.999999999999997335 ) ;
#16455=ORIENTED_EDGE ( 'NONE', *, *, #5272, .F. ) ;
#16461=CIRCLE ( 'NONE', #4655, 3.299999999999997158 ) ;
#16462=LINE ( 'NONE', #15267, #16360 ) ;
#16463=CARTESIAN_POINT ( 'NONE',  ( 31.81980515339464333, 8.000000000000000000, -28.51980515339463906 ) ) ;
#16467=DIRECTION ( 'NONE',  ( 0.000000000000000000, 1.000000000000000000, 0.000000000000000000 ) ) ;
#16472=ORIENTED_EDGE ( 'NONE', *, *, #686, .T. ) ;
#16478=CARTESIAN_POINT ( 'NONE',  ( -31.81980515339462912, 11.00000000000000000, -35.11980515339465114 ) ) ;
#16513=CARTESIAN_POINT ( 'NONE',  ( -20.99999999999999645, 19.00000000000000000, 35.00000000000001421 ) ) ;
#16524=CARTESIAN_POINT ( 'NONE',  ( -31.00000000000003553, 19.00000000000000000, -21.00000000000000000 ) ) ;
#16531=EDGE_CURVE ( 'NONE', #11631, #7648, #4008, .T. ) ;
#16538=DIRECTION ( 'NONE',  ( 1.000000000000000000, -0.000000000000000000, 0.000000000000000000 ) ) ;
#16550=AXIS2_PLACEMENT_3D ( 'NONE', #14146, #10284, #2444 ) ;
#16561=VECTOR ( 'NONE', #9132, 1000.000000000000000 ) ;
#16575=DIRECTION ( 'NONE',  ( 3.854941057726251409E-16, 0.000000000000000000, 1.000000000000000000 ) ) ;
#16586=ORIENTED_EDGE ( 'NONE', *, *, #16059, .F. ) ;
#16588=LINE ( 'NONE', #4817, #13567 ) ;
#16592=DIRECTION ( 'NONE',  ( -0.000000000000000000, -1.000000000000000000, -0.000000000000000000 ) ) ;
#16607=ADVANCED_FACE ( 'NONE', ( #9248 ), #8909, .F. ) ;
#16609=EDGE_CURVE ( 'NONE', #11059, #1839, #14089, .T. ) ;
#16612=DIRECTION ( 'NONE',  ( -0.000000000000000000, -1.000000000000000000, -0.000000000000000000 ) ) ;
#16615=AXIS2_PLACEMENT_3D ( 'NONE', #13447, #1669, #16176 ) ;
#16617=VERTEX_POINT ( 'NONE', #6902 ) ;
#16618=ORIENTED_EDGE ( 'NONE', *, *, #7517, .T. ) ;
#16624=PLANE ( 'NONE',  #6658 ) ;
#16625=AXIS2_PLACEMENT_3D ( 'NONE', #11243, #1971, #15206 ) ;
#16657=ADVANCED_FACE ( 'NONE', ( #14743 ), #2882, .F. ) ;
#16660=ADVANCED_FACE ( 'NONE', ( #4428 ), #9675, .F. ) ;
#16666=CARTESIAN_POINT ( 'NONE',  ( -31.81980515339462912, 8.000000000000000000, -31.81980515339465043 ) ) ;
#16674=ORIENTED_EDGE ( 'NONE', *, *, #12150, .T. ) ;
#16710=VECTOR ( 'NONE', #1457, 1000.000000000000000 ) ;
#16733=CARTESIAN_POINT ( 'NONE',  ( 31.00000000000000000, 19.00000000000000000, 30.99999999999999289 ) ) ;
#16739=ORIENTED_EDGE ( 'NONE', *, *, #14583, .F. ) ;
#16742=FACE_OUTER_BOUND ( 'NONE', #603, .T. ) ;
#16743=ADVANCED_FACE ( 'NONE', ( #4660 ), #8798, .T. ) ;
#16748=DIRECTION ( 'NONE',  ( 0.000000000000000000, 0.000000000000000000, -1.000000000000000000 ) ) ;
#16766=AXIS2_PLACEMENT_3D ( 'NONE', #4329, #16081, #12303 ) ;
#16796=CARTESIAN_POINT ( 'NONE',  ( 2.265596578422603396E-15, 8.000000000000000000, 18.50000000000000000 ) ) ;
#16804=VECTOR ( 'NONE', #6035, 1000.000000000000000 ) ;
#16813=DIRECTION ( 'NONE',  ( -0.000000000000000000, -1.000000000000000000, -0.000000000000000000 ) ) ;
#16823=ORIENTED_EDGE ( 'NONE', *, *, #10574, .T. ) ;
#16828=FACE_OUTER_BOUND ( 'NONE', #4549, .T. ) ;
#16829=VERTEX_POINT ( 'NONE', #12326 ) ;
#16830=DIRECTION ( 'NONE',  ( 0.000000000000000000, 1.000000000000000000, 0.000000000000000000 ) ) ;
#16840=CARTESIAN_POINT ( 'NONE',  ( -20.99999999999999645, 19.00000000000000000, -31.00000000000003908 ) ) ;
#16842=ORIENTED_EDGE ( 'NONE', *, *, #1177, .F. ) ;
#16844=EDGE_CURVE ( 'NONE', #10385, #394, #3392, .T. ) ;
#16861=DIRECTION ( 'NONE',  ( -0.000000000000000000, -1.000000000000000000, -0.000000000000000000 ) ) ;
#16862=ORIENTED_EDGE ( 'NONE', *, *, #13536, .T. ) ;
#16867=VECTOR ( 'NONE', #12672, 1000.000000000000000 ) ;
#16870=VERTEX_POINT ( 'NONE', #2008 ) ;
#16881=CARTESIAN_POINT ( 'NONE',  ( -20.99999999999999645, 19.00000000000000000, -35.00000000000000711 ) ) ;
#16882=VERTEX_POINT ( 'NONE', #7240 ) ;
#16889=ORIENTED_EDGE ( 'NONE', *, *, #10223, .T. ) ;
#16901=CARTESIAN_POINT ( 'NONE',  ( -26.00000000000000000, 19.00000000000000000, 40.00000000000001421 ) ) ;
#16910=DIRECTION ( 'NONE',  ( 0.000000000000000000, 0.000000000000000000, -1.000000000000000000 ) ) ;
#16919=EDGE_LOOP ( 'NONE', ( #12714, #7054, #12556, #1671, #15986, #1478 ) ) ;
#16924=VERTEX_POINT ( 'NONE', #10169 ) ;
#16935=EDGE_CURVE ( 'NONE', #15084, #3282, #8968, .T. ) ;
#16936=DIRECTION ( 'NONE',  ( -0.000000000000000000, -1.000000000000000000, -0.000000000000000000 ) ) ;
#16937=ORIENTED_EDGE ( 'NONE', *, *, #13061, .F. ) ;
#16942=ORIENTED_EDGE ( 'NONE', *, *, #9569, .F. ) ;
#16949=LINE ( 'NONE', #4004, #597 ) ;
#16951=EDGE_LOOP ( 'NONE', ( #16937, #11705, #154, #9881 ) ) ;
#16963=VECTOR ( 'NONE', #251, 1000.000000000000000 ) ;
ENDSEC;
END-ISO-10303-21;
